ISO-10303-21;
HEADER;
/* Generated by software containing ST-Developer
 * from STEP Tools, Inc. (www.steptools.com) 
 */

FILE_DESCRIPTION(
/* description */ (''),
/* implementation_level */ '2;1');

FILE_NAME(
/* name */ 'Bearing_04.step',
/* time_stamp */ '2026-10-05T21:54:13-07:00',
/* author */ (''),
/* organization */ (''),
/* preprocessor_version */ 'ST-DEVELOPER v20.2',
/* originating_system */ 'Autodesk Translation Framework v15.15.0.0',
/* authorisation */ '');

FILE_SCHEMA (('AUTOMOTIVE_DESIGN { 1 0 10303 214 3 1 1 }'));
ENDSEC;

DATA;
#10=MECHANICAL_DESIGN_GEOMETRIC_PRESENTATION_REPRESENTATION('',(#223,#224,#225,#226,#227,#228,#229,#230,#231,#232),#43781);
#85=SPHERICAL_SURFACE('',#14593,3.56616156686793);
#86=SPHERICAL_SURFACE('',#14595,3.56616156686793);
#87=SPHERICAL_SURFACE('',#14597,3.56616156686793);
#88=SPHERICAL_SURFACE('',#14599,3.56616156686793);
#89=SPHERICAL_SURFACE('',#14601,3.56616156686793);
#90=SPHERICAL_SURFACE('',#14603,3.56616156686793);
#91=SPHERICAL_SURFACE('',#14605,3.56616156686793);
#92=SPHERICAL_SURFACE('',#14659,3.56616156686792);
#93=SPHERICAL_SURFACE('',#14673,3.56616156686792);
#94=SPHERICAL_SURFACE('',#14687,3.56616156686792);
#95=SPHERICAL_SURFACE('',#14701,3.56616156686792);
#96=SPHERICAL_SURFACE('',#14715,3.56616156686792);
#97=SPHERICAL_SURFACE('',#14729,3.56616156686792);
#98=SPHERICAL_SURFACE('',#14739,3.56616156686792);
#111=CONICAL_SURFACE('',#14582,8.14999999999999,0.785398163397436);
#112=CONICAL_SURFACE('',#14585,7.5,0.785398163397437);
#113=CONICAL_SURFACE('',#14641,20.35,0.785398163397442);
#114=CONICAL_SURFACE('',#14644,21.,0.785398163397442);
#160=TOROIDAL_SURFACE('',#14567,14.25,3.56616156686793);
#161=TOROIDAL_SURFACE('',#14571,7.9875,0.4875);
#162=TOROIDAL_SURFACE('',#14577,7.9875,0.4875);
#163=TOROIDAL_SURFACE('',#14607,16.3271153846154,0.0585);
#164=TOROIDAL_SURFACE('',#14612,16.0931153846154,0.0585);
#165=TOROIDAL_SURFACE('',#14616,16.3271153846154,0.0585);
#166=TOROIDAL_SURFACE('',#14620,16.0931153846154,0.0585);
#167=TOROIDAL_SURFACE('',#14632,14.25,3.56616156686793);
#168=TOROIDAL_SURFACE('',#14655,2.5198520116158,1.69469015025);
#169=TOROIDAL_SURFACE('',#14669,2.5198520116158,1.69469015025);
#170=TOROIDAL_SURFACE('',#14683,2.5198520116158,1.69469015025);
#171=TOROIDAL_SURFACE('',#14697,2.5198520116158,1.69469015025);
#172=TOROIDAL_SURFACE('',#14711,2.5198520116158,1.69469015025);
#173=TOROIDAL_SURFACE('',#14725,2.5198520116158,1.69469015025);
#174=TOROIDAL_SURFACE('',#14749,2.5198520116158,1.69469015025);
#180=SHAPE_REPRESENTATION_RELATIONSHIP('SRR','None',#43818,#188);
#188=ADVANCED_BREP_SHAPE_REPRESENTATION('',(#267,#268,#269,#270,#271,#272,
#273,#274,#275,#276),#43778);
#223=STYLED_ITEM('',(#43863),#267);
#224=STYLED_ITEM('',(#43863),#268);
#225=STYLED_ITEM('',(#43863),#269);
#226=STYLED_ITEM('',(#43863),#270);
#227=STYLED_ITEM('',(#43863),#271);
#228=STYLED_ITEM('',(#43863),#272);
#229=STYLED_ITEM('',(#43863),#273);
#230=STYLED_ITEM('',(#43863),#274);
#231=STYLED_ITEM('',(#43863),#275);
#232=STYLED_ITEM('',(#43863),#276);
#267=MANIFOLD_SOLID_BREP('Body1',#13083);
#268=MANIFOLD_SOLID_BREP('Body2',#13084);
#269=MANIFOLD_SOLID_BREP('Body3',#13085);
#270=MANIFOLD_SOLID_BREP('Body4',#13086);
#271=MANIFOLD_SOLID_BREP('Body5',#13087);
#272=MANIFOLD_SOLID_BREP('Body6',#13088);
#273=MANIFOLD_SOLID_BREP('Body7',#13089);
#274=MANIFOLD_SOLID_BREP('Body8',#13090);
#275=MANIFOLD_SOLID_BREP('Body9',#13091);
#276=MANIFOLD_SOLID_BREP('Body10',#13092);
#433=FACE_BOUND('',#2817,.T.);
#434=FACE_BOUND('',#2819,.T.);
#435=FACE_BOUND('',#2842,.T.);
#436=FACE_BOUND('',#2844,.T.);
#437=FACE_BOUND('',#2846,.T.);
#438=FACE_BOUND('',#2848,.T.);
#439=FACE_BOUND('',#2850,.T.);
#440=FACE_BOUND('',#2852,.T.);
#441=FACE_BOUND('',#2854,.T.);
#442=FACE_BOUND('',#2855,.T.);
#443=FACE_BOUND('',#2857,.T.);
#444=FACE_BOUND('',#2858,.T.);
#445=FACE_BOUND('',#2860,.T.);
#446=FACE_BOUND('',#2861,.T.);
#447=FACE_BOUND('',#2863,.T.);
#448=FACE_BOUND('',#2864,.T.);
#449=FACE_BOUND('',#2866,.T.);
#450=FACE_BOUND('',#2867,.T.);
#451=FACE_BOUND('',#2869,.T.);
#452=FACE_BOUND('',#2870,.T.);
#453=FACE_BOUND('',#2872,.T.);
#454=FACE_BOUND('',#2873,.T.);
#455=FACE_BOUND('',#2875,.T.);
#456=FACE_BOUND('',#2876,.T.);
#457=FACE_BOUND('',#2878,.T.);
#458=FACE_BOUND('',#2879,.T.);
#459=FACE_BOUND('',#2881,.T.);
#460=FACE_BOUND('',#2882,.T.);
#461=FACE_BOUND('',#2884,.T.);
#462=FACE_BOUND('',#2885,.T.);
#463=FACE_BOUND('',#2887,.T.);
#464=FACE_BOUND('',#2888,.T.);
#465=FACE_BOUND('',#2890,.T.);
#466=FACE_BOUND('',#2891,.T.);
#467=FACE_BOUND('',#2893,.T.);
#468=FACE_BOUND('',#2894,.T.);
#469=FACE_BOUND('',#2900,.T.);
#470=FACE_BOUND('',#2902,.T.);
#471=FACE_BOUND('',#2908,.T.);
#472=FACE_BOUND('',#2910,.T.);
#473=FACE_BOUND('',#2920,.T.);
#474=FACE_BOUND('',#2922,.T.);
#475=FACE_BOUND('',#2932,.T.);
#476=FACE_BOUND('',#2934,.T.);
#477=FACE_BOUND('',#2944,.T.);
#478=FACE_BOUND('',#2946,.T.);
#479=FACE_BOUND('',#2956,.T.);
#480=FACE_BOUND('',#2958,.T.);
#481=FACE_BOUND('',#2968,.T.);
#482=FACE_BOUND('',#2970,.T.);
#863=B_SPLINE_CURVE_WITH_KNOTS('',3,(#42424,#42425,#42426,#42427,#42428,
#42429),.UNSPECIFIED.,.F.,.F.,(4,2,4),(0.436494357616827,0.49057908163088,
0.523269669927392),.UNSPECIFIED.);
#864=B_SPLINE_CURVE_WITH_KNOTS('',3,(#42431,#42432,#42433,#42434,#42435,
#42436,#42437,#42438,#42439,#42440,#42441,#42442,#42443,#42444,#42445,#42446,
#42447,#42448,#42449),.UNSPECIFIED.,.F.,.F.,(4,3,3,3,3,3,4),(-1.40481265039417,
-1.36522996541144,-1.32585540726346,-1.28679683363995,-1.26015734748852,
-1.21999608757349,-1.1843388203003),.UNSPECIFIED.);
#865=B_SPLINE_CURVE_WITH_KNOTS('',3,(#42451,#42452,#42453,#42454,#42455,
#42456),.UNSPECIFIED.,.F.,.F.,(4,2,4),(0.436494357616828,0.49057908163088,
0.523269669927516),.UNSPECIFIED.);
#866=B_SPLINE_CURVE_WITH_KNOTS('',3,(#42457,#42458,#42459,#42460,#42461,
#42462,#42463,#42464,#42465,#42466,#42467,#42468,#42469,#42470,#42471,#42472,
#42473,#42474,#42475),.UNSPECIFIED.,.F.,.F.,(4,3,3,3,3,3,4),(1.21344063784114,
1.25510987200879,1.29073244309217,1.33189452838103,1.37317594357341,1.41463545273866,
1.43283480298246),.UNSPECIFIED.);
#867=B_SPLINE_CURVE_WITH_KNOTS('',3,(#42478,#42479,#42480,#42481,#42482,
#42483),.UNSPECIFIED.,.F.,.F.,(4,2,4),(1.43904665659616,1.47173724489264,
1.52582196890669),.UNSPECIFIED.);
#868=B_SPLINE_CURVE_WITH_KNOTS('',3,(#42485,#42486,#42487,#42488,#42489,
#42490,#42491,#42492,#42493,#42494,#42495,#42496,#42497,#42498,#42499,#42500,
#42501,#42502,#42503),.UNSPECIFIED.,.F.,.F.,(4,3,3,3,3,3,4),(2.53632937909178,
2.57775416224765,2.61898206719527,2.6459019021663,2.68717408326041,2.72876559667488,
2.75562831582286),.UNSPECIFIED.);
#869=B_SPLINE_CURVE_WITH_KNOTS('',3,(#42505,#42506,#42507,#42508,#42509,
#42510),.UNSPECIFIED.,.F.,.F.,(4,2,4),(1.43904665659616,1.47173724489264,
1.52582196890582),.UNSPECIFIED.);
#870=B_SPLINE_CURVE_WITH_KNOTS('',3,(#42511,#42512,#42513,#42514,#42515,
#42516,#42517,#42518,#42519,#42520,#42521,#42522,#42523,#42524,#42525,#42526,
#42527,#42528,#42529),.UNSPECIFIED.,.F.,.F.,(4,3,3,3,3,3,4),(-0.110253525235352,
-0.070240741437667,-0.0308586443223014,0.,0.0392000421916667,0.0788707706427855,
0.110060546834446),.UNSPECIFIED.);
#871=B_SPLINE_CURVE_WITH_KNOTS('',3,(#42535,#42536,#42537,#42538,#42539,
#42540),.UNSPECIFIED.,.F.,.F.,(4,2,4),(-1.15327512303049,-1.04744023087766,
-0.941605338724827),.UNSPECIFIED.);
#872=B_SPLINE_CURVE_WITH_KNOTS('',3,(#42544,#42545,#42546,#42547,#42548,
#42549),.UNSPECIFIED.,.F.,.F.,(4,2,4),(0.959836356712345,1.06544831446544,
1.17106027221854),.UNSPECIFIED.);
#873=B_SPLINE_CURVE_WITH_KNOTS('',3,(#42556,#42557,#42558,#42559,#42560,
#42561,#42562),.UNSPECIFIED.,.F.,.F.,(4,3,4),(2.02528467117779,2.13089662893088,
2.23650858668398),.UNSPECIFIED.);
#874=B_SPLINE_CURVE_WITH_KNOTS('',3,(#42566,#42567,#42568,#42569,#42570,
#42571,#42572),.UNSPECIFIED.,.F.,.F.,(4,3,4),(-0.105834892152833,0.,0.105834892152833),
 .UNSPECIFIED.);
#875=B_SPLINE_CURVE_WITH_KNOTS('',3,(#42586,#42587,#42588,#42589,#42590,
#42591),.UNSPECIFIED.,.F.,.F.,(4,2,4),(0.436494357616816,0.49057908163088,
0.523269669927352),.UNSPECIFIED.);
#876=B_SPLINE_CURVE_WITH_KNOTS('',3,(#42593,#42594,#42595,#42596,#42597,
#42598,#42599,#42600,#42601,#42602,#42603,#42604,#42605,#42606,#42607,#42608,
#42609,#42610,#42611),.UNSPECIFIED.,.F.,.F.,(4,3,3,3,3,3,4),(-1.40481265039413,
-1.36522996541145,-1.32585540726349,-1.28679683363998,-1.2601573474885,
-1.21999608757352,-1.18433882030031),.UNSPECIFIED.);
#877=B_SPLINE_CURVE_WITH_KNOTS('',3,(#42613,#42614,#42615,#42616,#42617,
#42618),.UNSPECIFIED.,.F.,.F.,(4,2,4),(0.436484426249651,0.490578640084517,
0.523250481795878),.UNSPECIFIED.);
#878=B_SPLINE_CURVE_WITH_KNOTS('',3,(#42619,#42620,#42621,#42622,#42623,
#42624,#42625,#42626,#42627,#42628,#42629,#42630,#42631,#42632,#42633,#42634,
#42635,#42636,#42637),.UNSPECIFIED.,.F.,.F.,(4,3,3,3,3,3,4),(1.21344063784117,
1.2551098720088,1.29073244309219,1.33189452838105,1.37317594357344,1.41463545273871,
1.43283480298249),.UNSPECIFIED.);
#879=B_SPLINE_CURVE_WITH_KNOTS('',3,(#42640,#42641,#42642,#42643,#42644,
#42645),.UNSPECIFIED.,.F.,.F.,(4,2,4),(1.43906407854219,1.47173592025355,
1.52583013408841),.UNSPECIFIED.);
#880=B_SPLINE_CURVE_WITH_KNOTS('',3,(#42647,#42648,#42649,#42650,#42651,
#42652,#42653,#42654,#42655,#42656,#42657,#42658,#42659,#42660,#42661,#42662,
#42663,#42664,#42665),.UNSPECIFIED.,.F.,.F.,(4,3,3,3,3,3,4),(2.53632937909181,
2.57775416224765,2.61898206719527,2.64590190216633,2.68717408326044,2.72876559667489,
2.75562831582288),.UNSPECIFIED.);
#881=B_SPLINE_CURVE_WITH_KNOTS('',3,(#42667,#42668,#42669,#42670,#42671,
#42672),.UNSPECIFIED.,.F.,.F.,(4,2,4),(1.43906407854219,1.47173592025355,
1.52583013408754),.UNSPECIFIED.);
#882=B_SPLINE_CURVE_WITH_KNOTS('',3,(#42673,#42674,#42675,#42676,#42677,
#42678,#42679,#42680,#42681,#42682,#42683,#42684,#42685,#42686,#42687,#42688,
#42689,#42690,#42691),.UNSPECIFIED.,.F.,.F.,(4,3,3,3,3,3,4),(-0.110253525235351,
-0.0702407414376934,-0.0308586443223274,0.,0.0392000421916682,0.0788707706427895,
0.110060546834446),.UNSPECIFIED.);
#883=B_SPLINE_CURVE_WITH_KNOTS('',3,(#42697,#42698,#42699,#42700,#42701,
#42702),.UNSPECIFIED.,.F.,.F.,(4,2,4),(-1.15327512303049,-1.04744023087766,
-0.941605338724829),.UNSPECIFIED.);
#884=B_SPLINE_CURVE_WITH_KNOTS('',3,(#42706,#42707,#42708,#42709,#42710,
#42711),.UNSPECIFIED.,.F.,.F.,(4,2,4),(0.959836356712343,1.06544831446544,
1.17106027221854),.UNSPECIFIED.);
#885=B_SPLINE_CURVE_WITH_KNOTS('',3,(#42718,#42719,#42720,#42721,#42722,
#42723,#42724),.UNSPECIFIED.,.F.,.F.,(4,3,4),(2.02528467117778,2.13089662893088,
2.23650858668398),.UNSPECIFIED.);
#886=B_SPLINE_CURVE_WITH_KNOTS('',3,(#42728,#42729,#42730,#42731,#42732,
#42733,#42734),.UNSPECIFIED.,.F.,.F.,(4,3,4),(-0.105834892152834,0.,0.105834892152833),
 .UNSPECIFIED.);
#887=B_SPLINE_CURVE_WITH_KNOTS('',3,(#42748,#42749,#42750,#42751,#42752,
#42753),.UNSPECIFIED.,.F.,.F.,(4,2,4),(0.436484426249655,0.490578640084517,
0.523250481795882),.UNSPECIFIED.);
#888=B_SPLINE_CURVE_WITH_KNOTS('',3,(#42755,#42756,#42757,#42758,#42759,
#42760,#42761,#42762,#42763,#42764,#42765,#42766,#42767,#42768,#42769,#42770,
#42771,#42772,#42773),.UNSPECIFIED.,.F.,.F.,(4,3,3,3,3,3,4),(-0.110253525235353,
-0.0702407414376493,-0.0308586443222864,0.,0.0392000421916586,0.0788707706427754,
0.110060546834447),.UNSPECIFIED.);
#889=B_SPLINE_CURVE_WITH_KNOTS('',3,(#42775,#42776,#42777,#42778,#42779,
#42780),.UNSPECIFIED.,.F.,.F.,(4,2,4),(0.436494357616821,0.49057908163088,
0.523269669927365),.UNSPECIFIED.);
#890=B_SPLINE_CURVE_WITH_KNOTS('',3,(#42781,#42782,#42783,#42784,#42785,
#42786,#42787,#42788,#42789,#42790,#42791,#42792,#42793,#42794,#42795,#42796,
#42797,#42798,#42799),.UNSPECIFIED.,.F.,.F.,(4,3,3,3,3,3,4),(2.53632937909178,
2.57775416224762,2.61898206719525,2.64590190216632,2.68717408326042,2.72876559667488,
2.75562831582289),.UNSPECIFIED.);
#891=B_SPLINE_CURVE_WITH_KNOTS('',3,(#42802,#42803,#42804,#42805,#42806,
#42807),.UNSPECIFIED.,.F.,.F.,(4,2,4),(1.43906407854219,1.47173592025355,
1.52583013408841),.UNSPECIFIED.);
#892=B_SPLINE_CURVE_WITH_KNOTS('',3,(#42809,#42810,#42811,#42812,#42813,
#42814,#42815,#42816,#42817,#42818,#42819,#42820,#42821,#42822,#42823,#42824,
#42825,#42826,#42827),.UNSPECIFIED.,.F.,.F.,(4,3,3,3,3,3,4),(1.21344063784118,
1.25510987200885,1.29073244309219,1.33189452838105,1.37317594357345,1.41463545273868,
1.43283480298247),.UNSPECIFIED.);
#893=B_SPLINE_CURVE_WITH_KNOTS('',3,(#42829,#42830,#42831,#42832,#42833,
#42834),.UNSPECIFIED.,.F.,.F.,(4,2,4),(1.43906407854219,1.47173592025355,
1.52583013408753),.UNSPECIFIED.);
#894=B_SPLINE_CURVE_WITH_KNOTS('',3,(#42835,#42836,#42837,#42838,#42839,
#42840,#42841,#42842,#42843,#42844,#42845,#42846,#42847,#42848,#42849,#42850,
#42851,#42852,#42853),.UNSPECIFIED.,.F.,.F.,(4,3,3,3,3,3,4),(-1.40481265039415,
-1.36522996541142,-1.32585540726345,-1.28679683363994,-1.26015734748852,
-1.21999608757345,-1.18433882030032),.UNSPECIFIED.);
#895=B_SPLINE_CURVE_WITH_KNOTS('',3,(#42859,#42860,#42861,#42862,#42863,
#42864),.UNSPECIFIED.,.F.,.F.,(4,2,4),(-1.15327512303049,-1.04744023087766,
-0.941605338724827),.UNSPECIFIED.);
#896=B_SPLINE_CURVE_WITH_KNOTS('',3,(#42868,#42869,#42870,#42871,#42872,
#42873),.UNSPECIFIED.,.F.,.F.,(4,2,4),(0.959836356712344,1.06544831446544,
1.17106027221854),.UNSPECIFIED.);
#897=B_SPLINE_CURVE_WITH_KNOTS('',3,(#42880,#42881,#42882,#42883,#42884,
#42885,#42886),.UNSPECIFIED.,.F.,.F.,(4,3,4),(2.02528467117779,2.13089662893088,
2.23650858668398),.UNSPECIFIED.);
#898=B_SPLINE_CURVE_WITH_KNOTS('',3,(#42890,#42891,#42892,#42893,#42894,
#42895,#42896),.UNSPECIFIED.,.F.,.F.,(4,3,4),(-0.105834892152832,0.,0.105834892152832),
 .UNSPECIFIED.);
#899=B_SPLINE_CURVE_WITH_KNOTS('',3,(#42910,#42911,#42912,#42913,#42914,
#42915),.UNSPECIFIED.,.F.,.F.,(4,2,4),(0.436494357616822,0.49057908163088,
0.523269669927398),.UNSPECIFIED.);
#900=B_SPLINE_CURVE_WITH_KNOTS('',3,(#42917,#42918,#42919,#42920,#42921,
#42922,#42923,#42924,#42925,#42926,#42927,#42928,#42929,#42930,#42931,#42932,
#42933,#42934,#42935),.UNSPECIFIED.,.F.,.F.,(4,3,3,3,3,3,4),(-0.110253525235377,
-0.070240741437708,-0.0308586443223363,0.,0.03920004219167,0.0788707706428437,
0.110060546834472),.UNSPECIFIED.);
#901=B_SPLINE_CURVE_WITH_KNOTS('',3,(#42937,#42938,#42939,#42940,#42941,
#42942),.UNSPECIFIED.,.F.,.F.,(4,2,4),(0.436484426249657,0.490578640084517,
0.523250481796065),.UNSPECIFIED.);
#902=B_SPLINE_CURVE_WITH_KNOTS('',3,(#42943,#42944,#42945,#42946,#42947,
#42948,#42949,#42950,#42951,#42952,#42953,#42954,#42955,#42956,#42957,#42958,
#42959,#42960,#42961),.UNSPECIFIED.,.F.,.F.,(4,3,3,3,3,3,4),(2.53632937909185,
2.57775416224773,2.61898206719535,2.64590190216638,2.6871740832605,2.72876559667492,
2.75562831582295),.UNSPECIFIED.);
#903=B_SPLINE_CURVE_WITH_KNOTS('',3,(#42964,#42965,#42966,#42967,#42968,
#42969),.UNSPECIFIED.,.F.,.F.,(4,2,4),(1.43904665659616,1.47173724489264,
1.52582196890669),.UNSPECIFIED.);
#904=B_SPLINE_CURVE_WITH_KNOTS('',3,(#42971,#42972,#42973,#42974,#42975,
#42976,#42977,#42978,#42979,#42980,#42981,#42982,#42983,#42984,#42985,#42986,
#42987,#42988,#42989),.UNSPECIFIED.,.F.,.F.,(4,3,3,3,3,3,4),(1.2134406378412,
1.25510987200883,1.29073244309221,1.33189452838107,1.37317594357346,1.41463545273868,
1.43283480298249),.UNSPECIFIED.);
#905=B_SPLINE_CURVE_WITH_KNOTS('',3,(#42991,#42992,#42993,#42994,#42995,
#42996),.UNSPECIFIED.,.F.,.F.,(4,2,4),(1.43904665659616,1.47173724489264,
1.52582196890583),.UNSPECIFIED.);
#906=B_SPLINE_CURVE_WITH_KNOTS('',3,(#42997,#42998,#42999,#43000,#43001,
#43002,#43003,#43004,#43005,#43006,#43007,#43008,#43009,#43010,#43011,#43012,
#43013,#43014,#43015),.UNSPECIFIED.,.F.,.F.,(4,3,3,3,3,3,4),(-1.40481265039411,
-1.36522996541141,-1.32585540726345,-1.28679683363994,-1.26015734748849,
-1.21999608757351,-1.1843388203003),.UNSPECIFIED.);
#907=B_SPLINE_CURVE_WITH_KNOTS('',3,(#43021,#43022,#43023,#43024,#43025,
#43026),.UNSPECIFIED.,.F.,.F.,(4,2,4),(-1.15327512303049,-1.04744023087766,
-0.941605338724826),.UNSPECIFIED.);
#908=B_SPLINE_CURVE_WITH_KNOTS('',3,(#43030,#43031,#43032,#43033,#43034,
#43035),.UNSPECIFIED.,.F.,.F.,(4,2,4),(0.959836356712345,1.06544831446544,
1.17106027221854),.UNSPECIFIED.);
#909=B_SPLINE_CURVE_WITH_KNOTS('',3,(#43042,#43043,#43044,#43045,#43046,
#43047,#43048),.UNSPECIFIED.,.F.,.F.,(4,3,4),(2.02528467117779,2.13089662893088,
2.23650858668398),.UNSPECIFIED.);
#910=B_SPLINE_CURVE_WITH_KNOTS('',3,(#43052,#43053,#43054,#43055,#43056,
#43057,#43058),.UNSPECIFIED.,.F.,.F.,(4,3,4),(-0.105834892152833,0.,0.105834892152832),
 .UNSPECIFIED.);
#911=B_SPLINE_CURVE_WITH_KNOTS('',3,(#43072,#43073,#43074,#43075,#43076,
#43077),.UNSPECIFIED.,.F.,.F.,(4,2,4),(0.436494357616821,0.49057908163088,
0.523269669927355),.UNSPECIFIED.);
#912=B_SPLINE_CURVE_WITH_KNOTS('',3,(#43079,#43080,#43081,#43082,#43083,
#43084,#43085,#43086,#43087,#43088,#43089,#43090,#43091,#43092,#43093,#43094,
#43095,#43096,#43097),.UNSPECIFIED.,.F.,.F.,(4,3,3,3,3,3,4),(-0.110253525235352,
-0.0702407414377446,-0.0308586443223844,0.,0.039200042191676,0.0788707706427867,
0.110060546834448),.UNSPECIFIED.);
#913=B_SPLINE_CURVE_WITH_KNOTS('',3,(#43099,#43100,#43101,#43102,#43103,
#43104),.UNSPECIFIED.,.F.,.F.,(4,2,4),(0.436494357616821,0.49057908163088,
0.523269669927355),.UNSPECIFIED.);
#914=B_SPLINE_CURVE_WITH_KNOTS('',3,(#43105,#43106,#43107,#43108,#43109,
#43110,#43111,#43112,#43113,#43114,#43115,#43116,#43117,#43118,#43119,#43120,
#43121,#43122,#43123),.UNSPECIFIED.,.F.,.F.,(4,3,3,3,3,3,4),(2.53632937909179,
2.57775416224772,2.61898206719534,2.64590190216632,2.68717408326042,2.72876559667486,
2.75562831582289),.UNSPECIFIED.);
#915=B_SPLINE_CURVE_WITH_KNOTS('',3,(#43126,#43127,#43128,#43129,#43130,
#43131),.UNSPECIFIED.,.F.,.F.,(4,2,4),(1.43904665659616,1.47173724489264,
1.5258219689067),.UNSPECIFIED.);
#916=B_SPLINE_CURVE_WITH_KNOTS('',3,(#43133,#43134,#43135,#43136,#43137,
#43138,#43139,#43140,#43141,#43142,#43143,#43144,#43145,#43146,#43147,#43148,
#43149,#43150,#43151),.UNSPECIFIED.,.F.,.F.,(4,3,3,3,3,3,4),(1.21344063784118,
1.25510987200879,1.29073244309219,1.33189452838105,1.37317594357344,1.41463545273868,
1.43283480298247),.UNSPECIFIED.);
#917=B_SPLINE_CURVE_WITH_KNOTS('',3,(#43153,#43154,#43155,#43156,#43157,
#43158),.UNSPECIFIED.,.F.,.F.,(4,2,4),(1.43904665659616,1.47173724489264,
1.52582196890582),.UNSPECIFIED.);
#918=B_SPLINE_CURVE_WITH_KNOTS('',3,(#43159,#43160,#43161,#43162,#43163,
#43164,#43165,#43166,#43167,#43168,#43169,#43170,#43171,#43172,#43173,#43174,
#43175,#43176,#43177),.UNSPECIFIED.,.F.,.F.,(4,3,3,3,3,3,4),(-1.40481265039416,
-1.36522996541145,-1.32585540726348,-1.28679683363997,-1.26015734748853,
-1.21999608757355,-1.18433882030033),.UNSPECIFIED.);
#919=B_SPLINE_CURVE_WITH_KNOTS('',3,(#43183,#43184,#43185,#43186,#43187,
#43188),.UNSPECIFIED.,.F.,.F.,(4,2,4),(-1.15327512303049,-1.04744023087766,
-0.941605338724826),.UNSPECIFIED.);
#920=B_SPLINE_CURVE_WITH_KNOTS('',3,(#43192,#43193,#43194,#43195,#43196,
#43197),.UNSPECIFIED.,.F.,.F.,(4,2,4),(0.959836356712344,1.06544831446544,
1.17106027221854),.UNSPECIFIED.);
#921=B_SPLINE_CURVE_WITH_KNOTS('',3,(#43204,#43205,#43206,#43207,#43208,
#43209,#43210),.UNSPECIFIED.,.F.,.F.,(4,3,4),(2.02528467117778,2.13089662893088,
2.23650858668398),.UNSPECIFIED.);
#922=B_SPLINE_CURVE_WITH_KNOTS('',3,(#43214,#43215,#43216,#43217,#43218,
#43219,#43220),.UNSPECIFIED.,.F.,.F.,(4,3,4),(-0.105834892152833,0.,0.105834892152832),
 .UNSPECIFIED.);
#923=B_SPLINE_CURVE_WITH_KNOTS('',3,(#43234,#43235,#43236,#43237,#43238,
#43239,#43240,#43241,#43242,#43243,#43244,#43245,#43246,#43247,#43248,#43249,
#43250,#43251,#43252),.UNSPECIFIED.,.F.,.F.,(4,3,3,3,3,3,4),(2.47883976068978,
2.51859129056809,2.55786629068885,2.58890030752247,2.62818560996811,2.66809093310445,
2.69915383275782),.UNSPECIFIED.);
#924=B_SPLINE_CURVE_WITH_KNOTS('',3,(#43254,#43255,#43256,#43257,#43258,
#43259),.UNSPECIFIED.,.F.,.F.,(4,2,4),(-0.523250481795879,-0.490578640084517,
-0.43648442624966),.UNSPECIFIED.);
#925=B_SPLINE_CURVE_WITH_KNOTS('',3,(#43261,#43262,#43263,#43264,#43265,
#43266,#43267,#43268,#43269,#43270,#43271,#43272,#43273,#43274,#43275,#43276,
#43277,#43278,#43279),.UNSPECIFIED.,.F.,.F.,(4,3,3,3,3,3,4),(-0.109726413656553,
-0.0680893754924848,-0.0267736956128723,0.,0.0412006233150074,0.082597721206199,
0.109572523074534),.UNSPECIFIED.);
#926=B_SPLINE_CURVE_WITH_KNOTS('',3,(#43280,#43281,#43282,#43283,#43284,
#43285),.UNSPECIFIED.,.F.,.F.,(4,2,4),(-0.523250481795672,-0.490578640084517,
-0.436484426249653),.UNSPECIFIED.);
#927=B_SPLINE_CURVE_WITH_KNOTS('',3,(#43288,#43289,#43290,#43291,#43292,
#43293),.UNSPECIFIED.,.F.,.F.,(4,2,4),(1.43904665659616,1.47173724489264,
1.5258219689067),.UNSPECIFIED.);
#928=B_SPLINE_CURVE_WITH_KNOTS('',3,(#43295,#43296,#43297,#43298,#43299,
#43300,#43301,#43302,#43303,#43304,#43305,#43306,#43307,#43308,#43309,#43310,
#43311,#43312,#43313),.UNSPECIFIED.,.F.,.F.,(4,3,3,3,3,3,4),(1.21344063784118,
1.25510987200878,1.29073244309219,1.33189452838105,1.37317594357344,1.41463545273868,
1.43283480298247),.UNSPECIFIED.);
#929=B_SPLINE_CURVE_WITH_KNOTS('',3,(#43315,#43316,#43317,#43318,#43319,
#43320),.UNSPECIFIED.,.F.,.F.,(4,2,4),(1.43904665659617,1.47173724489264,
1.52582196890583),.UNSPECIFIED.);
#930=B_SPLINE_CURVE_WITH_KNOTS('',3,(#43321,#43322,#43323,#43324,#43325,
#43326,#43327,#43328,#43329,#43330,#43331,#43332,#43333,#43334,#43335,#43336,
#43337,#43338,#43339),.UNSPECIFIED.,.F.,.F.,(4,3,3,3,3,3,4),(-1.40481265039414,
-1.36522996541144,-1.32585540726348,-1.28679683363997,-1.26015734748851,
-1.21999608757358,-1.18433882030032),.UNSPECIFIED.);
#931=B_SPLINE_CURVE_WITH_KNOTS('',3,(#43349,#43350,#43351,#43352,#43353,
#43354,#43355),.UNSPECIFIED.,.F.,.F.,(4,3,4),(2.02528467117778,2.13089662893088,
2.23650858668398),.UNSPECIFIED.);
#932=B_SPLINE_CURVE_WITH_KNOTS('',3,(#43359,#43360,#43361,#43362,#43363,
#43364,#43365),.UNSPECIFIED.,.F.,.F.,(4,3,4),(-0.105834892152832,0.,0.105834892152832),
 .UNSPECIFIED.);
#933=B_SPLINE_CURVE_WITH_KNOTS('',3,(#43370,#43371,#43372,#43373,#43374,
#43375),.UNSPECIFIED.,.F.,.F.,(4,2,4),(0.941605338724826,1.04744023087766,
1.15327512303049),.UNSPECIFIED.);
#934=B_SPLINE_CURVE_WITH_KNOTS('',3,(#43378,#43379,#43380,#43381,#43382,
#43383),.UNSPECIFIED.,.F.,.F.,(4,2,4),(-1.17106027221854,-1.06544831446544,
-0.959836356712344),.UNSPECIFIED.);
#935=B_SPLINE_CURVE_WITH_KNOTS('',3,(#43393,#43394,#43395,#43396,#43397,
#43398),.UNSPECIFIED.,.F.,.F.,(4,2,4),(-1.15327512303049,-1.04744023087766,
-0.941605338724827),.UNSPECIFIED.);
#936=B_SPLINE_CURVE_WITH_KNOTS('',3,(#43402,#43403,#43404,#43405,#43406,
#43407),.UNSPECIFIED.,.F.,.F.,(4,2,4),(0.959836356712344,1.06544831446544,
1.17106027221854),.UNSPECIFIED.);
#937=B_SPLINE_CURVE_WITH_KNOTS('',3,(#43414,#43415,#43416,#43417,#43418,
#43419,#43420),.UNSPECIFIED.,.F.,.F.,(4,3,4),(2.02528467117778,2.13089662893088,
2.23650858668398),.UNSPECIFIED.);
#938=B_SPLINE_CURVE_WITH_KNOTS('',3,(#43424,#43425,#43426,#43427,#43428,
#43429,#43430),.UNSPECIFIED.,.F.,.F.,(4,3,4),(-0.105834892152833,0.,0.105834892152832),
 .UNSPECIFIED.);
#939=B_SPLINE_CURVE_WITH_KNOTS('',3,(#43444,#43445,#43446,#43447,#43448,
#43449),.UNSPECIFIED.,.F.,.F.,(4,2,4),(0.43648442624966,0.490578640084517,
0.523250481795913),.UNSPECIFIED.);
#940=B_SPLINE_CURVE_WITH_KNOTS('',3,(#43451,#43452,#43453,#43454,#43455,
#43456,#43457,#43458,#43459,#43460,#43461,#43462,#43463,#43464,#43465,#43466,
#43467,#43468,#43469),.UNSPECIFIED.,.F.,.F.,(4,3,3,3,3,3,4),(-1.40481265039423,
-1.36522996541152,-1.32585540726357,-1.28679683364005,-1.26015734748857,
-1.2199960875736,-1.18433882030035),.UNSPECIFIED.);
#941=B_SPLINE_CURVE_WITH_KNOTS('',3,(#43471,#43472,#43473,#43474,#43475,
#43476),.UNSPECIFIED.,.F.,.F.,(4,2,4),(0.436494357616825,0.49057908163088,
0.523269669927497),.UNSPECIFIED.);
#942=B_SPLINE_CURVE_WITH_KNOTS('',3,(#43477,#43478,#43479,#43480,#43481,
#43482,#43483,#43484,#43485,#43486,#43487,#43488,#43489,#43490,#43491,#43492,
#43493,#43494,#43495),.UNSPECIFIED.,.F.,.F.,(4,3,3,3,3,3,4),(1.21344063784115,
1.25510987200874,1.29073244309218,1.33189452838104,1.37317594357343,1.41463545273866,
1.43283480298248),.UNSPECIFIED.);
#943=B_SPLINE_CURVE_WITH_KNOTS('',3,(#43498,#43499,#43500,#43501,#43502,
#43503),.UNSPECIFIED.,.F.,.F.,(4,2,4),(1.43906407854219,1.47173592025355,
1.52583013408841),.UNSPECIFIED.);
#944=B_SPLINE_CURVE_WITH_KNOTS('',3,(#43505,#43506,#43507,#43508,#43509,
#43510,#43511,#43512,#43513,#43514,#43515,#43516,#43517,#43518,#43519,#43520,
#43521,#43522,#43523),.UNSPECIFIED.,.F.,.F.,(4,3,3,3,3,3,4),(2.53632937909179,
2.57775416224768,2.61898206719531,2.64590190216631,2.68717408326042,2.72876559667485,
2.75562831582286),.UNSPECIFIED.);
#945=B_SPLINE_CURVE_WITH_KNOTS('',3,(#43525,#43526,#43527,#43528,#43529,
#43530),.UNSPECIFIED.,.F.,.F.,(4,2,4),(1.43906407854219,1.47173592025355,
1.52583013408754),.UNSPECIFIED.);
#946=B_SPLINE_CURVE_WITH_KNOTS('',3,(#43531,#43532,#43533,#43534,#43535,
#43536,#43537,#43538,#43539,#43540,#43541,#43542,#43543,#43544,#43545,#43546,
#43547,#43548,#43549),.UNSPECIFIED.,.F.,.F.,(4,3,3,3,3,3,4),(-0.110253525235352,
-0.0702407414376601,-0.030858644322292,0.,0.0392000421916706,0.0788707706427867,
0.110060546834447),.UNSPECIFIED.);
#1225=PLANE('',#14591);
#1226=PLANE('',#14592);
#1227=PLANE('',#14649);
#1228=PLANE('',#14650);
#1229=PLANE('',#14651);
#1230=PLANE('',#14652);
#1231=PLANE('',#14653);
#1232=PLANE('',#14654);
#1233=PLANE('',#14759);
#1234=PLANE('',#14760);
#1235=PLANE('',#14761);
#1236=PLANE('',#14762);
#1237=PLANE('',#14763);
#1238=PLANE('',#14766);
#1239=PLANE('',#14771);
#1240=PLANE('',#14772);
#1241=PLANE('',#14773);
#1242=PLANE('',#14776);
#1243=PLANE('',#14787);
#1244=PLANE('',#14788);
#1245=PLANE('',#14789);
#1246=PLANE('',#14790);
#1247=PLANE('',#14791);
#1248=PLANE('',#14794);
#1249=PLANE('',#14805);
#1250=PLANE('',#14806);
#1251=PLANE('',#14807);
#1252=PLANE('',#14808);
#1253=PLANE('',#14809);
#1254=PLANE('',#14812);
#1255=PLANE('',#14823);
#1256=PLANE('',#14824);
#1257=PLANE('',#14825);
#1258=PLANE('',#14826);
#1259=PLANE('',#14827);
#1260=PLANE('',#14830);
#1261=PLANE('',#14841);
#1262=PLANE('',#14842);
#1263=PLANE('',#14843);
#1264=PLANE('',#14844);
#1265=PLANE('',#14845);
#1266=PLANE('',#14848);
#1267=PLANE('',#14859);
#1268=PLANE('',#14860);
#1269=PLANE('',#14861);
#1270=PLANE('',#14862);
#1271=PLANE('',#14863);
#1272=PLANE('',#14866);
#1273=PLANE('',#14871);
#1274=PLANE('',#14874);
#1902=FACE_OUTER_BOUND('',#2808,.T.);
#1903=FACE_OUTER_BOUND('',#2809,.T.);
#1904=FACE_OUTER_BOUND('',#2810,.T.);
#1905=FACE_OUTER_BOUND('',#2811,.T.);
#1906=FACE_OUTER_BOUND('',#2812,.T.);
#1907=FACE_OUTER_BOUND('',#2813,.T.);
#1908=FACE_OUTER_BOUND('',#2814,.T.);
#1909=FACE_OUTER_BOUND('',#2815,.T.);
#1910=FACE_OUTER_BOUND('',#2816,.T.);
#1911=FACE_OUTER_BOUND('',#2818,.T.);
#1912=FACE_OUTER_BOUND('',#2820,.T.);
#1913=FACE_OUTER_BOUND('',#2821,.T.);
#1914=FACE_OUTER_BOUND('',#2822,.T.);
#1915=FACE_OUTER_BOUND('',#2823,.T.);
#1916=FACE_OUTER_BOUND('',#2824,.T.);
#1917=FACE_OUTER_BOUND('',#2825,.T.);
#1918=FACE_OUTER_BOUND('',#2826,.T.);
#1919=FACE_OUTER_BOUND('',#2827,.T.);
#1920=FACE_OUTER_BOUND('',#2828,.T.);
#1921=FACE_OUTER_BOUND('',#2829,.T.);
#1922=FACE_OUTER_BOUND('',#2830,.T.);
#1923=FACE_OUTER_BOUND('',#2831,.T.);
#1924=FACE_OUTER_BOUND('',#2832,.T.);
#1925=FACE_OUTER_BOUND('',#2833,.T.);
#1926=FACE_OUTER_BOUND('',#2834,.T.);
#1927=FACE_OUTER_BOUND('',#2835,.T.);
#1928=FACE_OUTER_BOUND('',#2836,.T.);
#1929=FACE_OUTER_BOUND('',#2837,.T.);
#1930=FACE_OUTER_BOUND('',#2838,.T.);
#1931=FACE_OUTER_BOUND('',#2839,.T.);
#1932=FACE_OUTER_BOUND('',#2840,.T.);
#1933=FACE_OUTER_BOUND('',#2841,.T.);
#1934=FACE_OUTER_BOUND('',#2843,.T.);
#1935=FACE_OUTER_BOUND('',#2845,.T.);
#1936=FACE_OUTER_BOUND('',#2847,.T.);
#1937=FACE_OUTER_BOUND('',#2849,.T.);
#1938=FACE_OUTER_BOUND('',#2851,.T.);
#1939=FACE_OUTER_BOUND('',#2853,.T.);
#1940=FACE_OUTER_BOUND('',#2856,.T.);
#1941=FACE_OUTER_BOUND('',#2859,.T.);
#1942=FACE_OUTER_BOUND('',#2862,.T.);
#1943=FACE_OUTER_BOUND('',#2865,.T.);
#1944=FACE_OUTER_BOUND('',#2868,.T.);
#1945=FACE_OUTER_BOUND('',#2871,.T.);
#1946=FACE_OUTER_BOUND('',#2874,.T.);
#1947=FACE_OUTER_BOUND('',#2877,.T.);
#1948=FACE_OUTER_BOUND('',#2880,.T.);
#1949=FACE_OUTER_BOUND('',#2883,.T.);
#1950=FACE_OUTER_BOUND('',#2886,.T.);
#1951=FACE_OUTER_BOUND('',#2889,.T.);
#1952=FACE_OUTER_BOUND('',#2892,.T.);
#1953=FACE_OUTER_BOUND('',#2895,.T.);
#1954=FACE_OUTER_BOUND('',#2896,.T.);
#1955=FACE_OUTER_BOUND('',#2897,.T.);
#1956=FACE_OUTER_BOUND('',#2898,.T.);
#1957=FACE_OUTER_BOUND('',#2899,.T.);
#1958=FACE_OUTER_BOUND('',#2901,.T.);
#1959=FACE_OUTER_BOUND('',#2903,.T.);
#1960=FACE_OUTER_BOUND('',#2904,.T.);
#1961=FACE_OUTER_BOUND('',#2905,.T.);
#1962=FACE_OUTER_BOUND('',#2906,.T.);
#1963=FACE_OUTER_BOUND('',#2907,.T.);
#1964=FACE_OUTER_BOUND('',#2909,.T.);
#1965=FACE_OUTER_BOUND('',#2911,.T.);
#1966=FACE_OUTER_BOUND('',#2912,.T.);
#1967=FACE_OUTER_BOUND('',#2913,.T.);
#1968=FACE_OUTER_BOUND('',#2914,.T.);
#1969=FACE_OUTER_BOUND('',#2915,.T.);
#1970=FACE_OUTER_BOUND('',#2916,.T.);
#1971=FACE_OUTER_BOUND('',#2917,.T.);
#1972=FACE_OUTER_BOUND('',#2918,.T.);
#1973=FACE_OUTER_BOUND('',#2919,.T.);
#1974=FACE_OUTER_BOUND('',#2921,.T.);
#1975=FACE_OUTER_BOUND('',#2923,.T.);
#1976=FACE_OUTER_BOUND('',#2924,.T.);
#1977=FACE_OUTER_BOUND('',#2925,.T.);
#1978=FACE_OUTER_BOUND('',#2926,.T.);
#1979=FACE_OUTER_BOUND('',#2927,.T.);
#1980=FACE_OUTER_BOUND('',#2928,.T.);
#1981=FACE_OUTER_BOUND('',#2929,.T.);
#1982=FACE_OUTER_BOUND('',#2930,.T.);
#1983=FACE_OUTER_BOUND('',#2931,.T.);
#1984=FACE_OUTER_BOUND('',#2933,.T.);
#1985=FACE_OUTER_BOUND('',#2935,.T.);
#1986=FACE_OUTER_BOUND('',#2936,.T.);
#1987=FACE_OUTER_BOUND('',#2937,.T.);
#1988=FACE_OUTER_BOUND('',#2938,.T.);
#1989=FACE_OUTER_BOUND('',#2939,.T.);
#1990=FACE_OUTER_BOUND('',#2940,.T.);
#1991=FACE_OUTER_BOUND('',#2941,.T.);
#1992=FACE_OUTER_BOUND('',#2942,.T.);
#1993=FACE_OUTER_BOUND('',#2943,.T.);
#1994=FACE_OUTER_BOUND('',#2945,.T.);
#1995=FACE_OUTER_BOUND('',#2947,.T.);
#1996=FACE_OUTER_BOUND('',#2948,.T.);
#1997=FACE_OUTER_BOUND('',#2949,.T.);
#1998=FACE_OUTER_BOUND('',#2950,.T.);
#1999=FACE_OUTER_BOUND('',#2951,.T.);
#2000=FACE_OUTER_BOUND('',#2952,.T.);
#2001=FACE_OUTER_BOUND('',#2953,.T.);
#2002=FACE_OUTER_BOUND('',#2954,.T.);
#2003=FACE_OUTER_BOUND('',#2955,.T.);
#2004=FACE_OUTER_BOUND('',#2957,.T.);
#2005=FACE_OUTER_BOUND('',#2959,.T.);
#2006=FACE_OUTER_BOUND('',#2960,.T.);
#2007=FACE_OUTER_BOUND('',#2961,.T.);
#2008=FACE_OUTER_BOUND('',#2962,.T.);
#2009=FACE_OUTER_BOUND('',#2963,.T.);
#2010=FACE_OUTER_BOUND('',#2964,.T.);
#2011=FACE_OUTER_BOUND('',#2965,.T.);
#2012=FACE_OUTER_BOUND('',#2966,.T.);
#2013=FACE_OUTER_BOUND('',#2967,.T.);
#2014=FACE_OUTER_BOUND('',#2969,.T.);
#2015=FACE_OUTER_BOUND('',#2971,.T.);
#2016=FACE_OUTER_BOUND('',#2972,.T.);
#2017=FACE_OUTER_BOUND('',#2973,.T.);
#2018=FACE_OUTER_BOUND('',#2974,.T.);
#2019=FACE_OUTER_BOUND('',#2975,.T.);
#2020=FACE_OUTER_BOUND('',#2976,.T.);
#2021=FACE_OUTER_BOUND('',#2977,.T.);
#2022=FACE_OUTER_BOUND('',#2978,.T.);
#2808=EDGE_LOOP('',(#11369,#11370,#11371,#11372));
#2809=EDGE_LOOP('',(#11373,#11374,#11375,#11376,#11377,#11378));
#2810=EDGE_LOOP('',(#11379,#11380,#11381,#11382,#11383));
#2811=EDGE_LOOP('',(#11384,#11385,#11386,#11387,#11388));
#2812=EDGE_LOOP('',(#11389,#11390,#11391,#11392,#11393,#11394));
#2813=EDGE_LOOP('',(#11395,#11396,#11397,#11398));
#2814=EDGE_LOOP('',(#11399,#11400,#11401,#11402));
#2815=EDGE_LOOP('',(#11403,#11404,#11405,#11406));
#2816=EDGE_LOOP('',(#11407));
#2817=EDGE_LOOP('',(#11408));
#2818=EDGE_LOOP('',(#11409));
#2819=EDGE_LOOP('',(#11410));
#2820=EDGE_LOOP('',(#11411,#11412));
#2821=EDGE_LOOP('',(#11413,#11414));
#2822=EDGE_LOOP('',(#11415,#11416));
#2823=EDGE_LOOP('',(#11417,#11418));
#2824=EDGE_LOOP('',(#11419,#11420));
#2825=EDGE_LOOP('',(#11421,#11422));
#2826=EDGE_LOOP('',(#11423,#11424));
#2827=EDGE_LOOP('',(#11425,#11426,#11427,#11428,#11429));
#2828=EDGE_LOOP('',(#11430,#11431,#11432,#11433));
#2829=EDGE_LOOP('',(#11434,#11435,#11436,#11437));
#2830=EDGE_LOOP('',(#11438,#11439,#11440,#11441,#11442));
#2831=EDGE_LOOP('',(#11443,#11444,#11445,#11446));
#2832=EDGE_LOOP('',(#11447,#11448,#11449,#11450,#11451));
#2833=EDGE_LOOP('',(#11452,#11453,#11454,#11455,#11456));
#2834=EDGE_LOOP('',(#11457,#11458,#11459,#11460));
#2835=EDGE_LOOP('',(#11461,#11462,#11463,#11464));
#2836=EDGE_LOOP('',(#11465,#11466,#11467,#11468));
#2837=EDGE_LOOP('',(#11469,#11470,#11471,#11472));
#2838=EDGE_LOOP('',(#11473,#11474,#11475,#11476));
#2839=EDGE_LOOP('',(#11477,#11478,#11479,#11480,#11481));
#2840=EDGE_LOOP('',(#11482,#11483,#11484,#11485,#11486));
#2841=EDGE_LOOP('',(#11487));
#2842=EDGE_LOOP('',(#11488));
#2843=EDGE_LOOP('',(#11489));
#2844=EDGE_LOOP('',(#11490));
#2845=EDGE_LOOP('',(#11491));
#2846=EDGE_LOOP('',(#11492));
#2847=EDGE_LOOP('',(#11493));
#2848=EDGE_LOOP('',(#11494));
#2849=EDGE_LOOP('',(#11495));
#2850=EDGE_LOOP('',(#11496));
#2851=EDGE_LOOP('',(#11497));
#2852=EDGE_LOOP('',(#11498));
#2853=EDGE_LOOP('',(#11499,#11500,#11501,#11502));
#2854=EDGE_LOOP('',(#11503,#11504,#11505,#11506));
#2855=EDGE_LOOP('',(#11507,#11508,#11509,#11510));
#2856=EDGE_LOOP('',(#11511,#11512,#11513,#11514,#11515,#11516,#11517,#11518,
#11519,#11520,#11521,#11522));
#2857=EDGE_LOOP('',(#11523));
#2858=EDGE_LOOP('',(#11524));
#2859=EDGE_LOOP('',(#11525,#11526,#11527,#11528));
#2860=EDGE_LOOP('',(#11529,#11530,#11531,#11532));
#2861=EDGE_LOOP('',(#11533,#11534,#11535,#11536));
#2862=EDGE_LOOP('',(#11537,#11538,#11539,#11540,#11541,#11542,#11543,#11544,
#11545,#11546,#11547,#11548));
#2863=EDGE_LOOP('',(#11549));
#2864=EDGE_LOOP('',(#11550));
#2865=EDGE_LOOP('',(#11551,#11552,#11553,#11554));
#2866=EDGE_LOOP('',(#11555,#11556,#11557,#11558));
#2867=EDGE_LOOP('',(#11559,#11560,#11561,#11562));
#2868=EDGE_LOOP('',(#11563,#11564,#11565,#11566,#11567,#11568,#11569,#11570,
#11571,#11572,#11573,#11574));
#2869=EDGE_LOOP('',(#11575));
#2870=EDGE_LOOP('',(#11576));
#2871=EDGE_LOOP('',(#11577,#11578,#11579,#11580));
#2872=EDGE_LOOP('',(#11581,#11582,#11583,#11584));
#2873=EDGE_LOOP('',(#11585,#11586,#11587,#11588));
#2874=EDGE_LOOP('',(#11589,#11590,#11591,#11592,#11593,#11594,#11595,#11596,
#11597,#11598,#11599,#11600));
#2875=EDGE_LOOP('',(#11601));
#2876=EDGE_LOOP('',(#11602));
#2877=EDGE_LOOP('',(#11603,#11604,#11605,#11606));
#2878=EDGE_LOOP('',(#11607,#11608,#11609,#11610));
#2879=EDGE_LOOP('',(#11611,#11612,#11613,#11614));
#2880=EDGE_LOOP('',(#11615,#11616,#11617,#11618,#11619,#11620,#11621,#11622,
#11623,#11624,#11625,#11626));
#2881=EDGE_LOOP('',(#11627));
#2882=EDGE_LOOP('',(#11628));
#2883=EDGE_LOOP('',(#11629,#11630,#11631,#11632));
#2884=EDGE_LOOP('',(#11633,#11634,#11635,#11636));
#2885=EDGE_LOOP('',(#11637,#11638,#11639,#11640));
#2886=EDGE_LOOP('',(#11641,#11642,#11643,#11644,#11645,#11646,#11647,#11648,
#11649,#11650,#11651,#11652));
#2887=EDGE_LOOP('',(#11653));
#2888=EDGE_LOOP('',(#11654));
#2889=EDGE_LOOP('',(#11655,#11656,#11657,#11658,#11659,#11660,#11661,#11662,
#11663,#11664,#11665,#11666));
#2890=EDGE_LOOP('',(#11667));
#2891=EDGE_LOOP('',(#11668));
#2892=EDGE_LOOP('',(#11669,#11670,#11671,#11672));
#2893=EDGE_LOOP('',(#11673,#11674,#11675,#11676));
#2894=EDGE_LOOP('',(#11677,#11678,#11679,#11680));
#2895=EDGE_LOOP('',(#11681,#11682,#11683,#11684));
#2896=EDGE_LOOP('',(#11685,#11686,#11687,#11688));
#2897=EDGE_LOOP('',(#11689,#11690,#11691,#11692));
#2898=EDGE_LOOP('',(#11693,#11694,#11695,#11696));
#2899=EDGE_LOOP('',(#11697));
#2900=EDGE_LOOP('',(#11698));
#2901=EDGE_LOOP('',(#11699));
#2902=EDGE_LOOP('',(#11700));
#2903=EDGE_LOOP('',(#11701,#11702,#11703,#11704));
#2904=EDGE_LOOP('',(#11705,#11706,#11707,#11708,#11709,#11710));
#2905=EDGE_LOOP('',(#11711,#11712,#11713,#11714));
#2906=EDGE_LOOP('',(#11715,#11716,#11717,#11718));
#2907=EDGE_LOOP('',(#11719));
#2908=EDGE_LOOP('',(#11720));
#2909=EDGE_LOOP('',(#11721));
#2910=EDGE_LOOP('',(#11722));
#2911=EDGE_LOOP('',(#11723,#11724,#11725,#11726));
#2912=EDGE_LOOP('',(#11727,#11728,#11729,#11730));
#2913=EDGE_LOOP('',(#11731,#11732,#11733,#11734));
#2914=EDGE_LOOP('',(#11735,#11736,#11737,#11738));
#2915=EDGE_LOOP('',(#11739,#11740,#11741,#11742));
#2916=EDGE_LOOP('',(#11743,#11744,#11745,#11746));
#2917=EDGE_LOOP('',(#11747,#11748,#11749,#11750,#11751,#11752));
#2918=EDGE_LOOP('',(#11753,#11754,#11755,#11756));
#2919=EDGE_LOOP('',(#11757));
#2920=EDGE_LOOP('',(#11758));
#2921=EDGE_LOOP('',(#11759));
#2922=EDGE_LOOP('',(#11760));
#2923=EDGE_LOOP('',(#11761,#11762,#11763,#11764));
#2924=EDGE_LOOP('',(#11765,#11766,#11767,#11768));
#2925=EDGE_LOOP('',(#11769,#11770,#11771,#11772));
#2926=EDGE_LOOP('',(#11773,#11774,#11775,#11776));
#2927=EDGE_LOOP('',(#11777,#11778,#11779,#11780));
#2928=EDGE_LOOP('',(#11781,#11782,#11783,#11784));
#2929=EDGE_LOOP('',(#11785,#11786,#11787,#11788,#11789,#11790));
#2930=EDGE_LOOP('',(#11791,#11792,#11793,#11794));
#2931=EDGE_LOOP('',(#11795));
#2932=EDGE_LOOP('',(#11796));
#2933=EDGE_LOOP('',(#11797));
#2934=EDGE_LOOP('',(#11798));
#2935=EDGE_LOOP('',(#11799,#11800,#11801,#11802));
#2936=EDGE_LOOP('',(#11803,#11804,#11805,#11806));
#2937=EDGE_LOOP('',(#11807,#11808,#11809,#11810));
#2938=EDGE_LOOP('',(#11811,#11812,#11813,#11814));
#2939=EDGE_LOOP('',(#11815,#11816,#11817,#11818));
#2940=EDGE_LOOP('',(#11819,#11820,#11821,#11822));
#2941=EDGE_LOOP('',(#11823,#11824,#11825,#11826,#11827,#11828));
#2942=EDGE_LOOP('',(#11829,#11830,#11831,#11832));
#2943=EDGE_LOOP('',(#11833));
#2944=EDGE_LOOP('',(#11834));
#2945=EDGE_LOOP('',(#11835));
#2946=EDGE_LOOP('',(#11836));
#2947=EDGE_LOOP('',(#11837,#11838,#11839,#11840));
#2948=EDGE_LOOP('',(#11841,#11842,#11843,#11844));
#2949=EDGE_LOOP('',(#11845,#11846,#11847,#11848));
#2950=EDGE_LOOP('',(#11849,#11850,#11851,#11852));
#2951=EDGE_LOOP('',(#11853,#11854,#11855,#11856));
#2952=EDGE_LOOP('',(#11857,#11858,#11859,#11860));
#2953=EDGE_LOOP('',(#11861,#11862,#11863,#11864,#11865,#11866));
#2954=EDGE_LOOP('',(#11867,#11868,#11869,#11870));
#2955=EDGE_LOOP('',(#11871));
#2956=EDGE_LOOP('',(#11872));
#2957=EDGE_LOOP('',(#11873));
#2958=EDGE_LOOP('',(#11874));
#2959=EDGE_LOOP('',(#11875,#11876,#11877,#11878));
#2960=EDGE_LOOP('',(#11879,#11880,#11881,#11882));
#2961=EDGE_LOOP('',(#11883,#11884,#11885,#11886));
#2962=EDGE_LOOP('',(#11887,#11888,#11889,#11890));
#2963=EDGE_LOOP('',(#11891,#11892,#11893,#11894));
#2964=EDGE_LOOP('',(#11895,#11896,#11897,#11898));
#2965=EDGE_LOOP('',(#11899,#11900,#11901,#11902,#11903,#11904));
#2966=EDGE_LOOP('',(#11905,#11906,#11907,#11908));
#2967=EDGE_LOOP('',(#11909));
#2968=EDGE_LOOP('',(#11910));
#2969=EDGE_LOOP('',(#11911));
#2970=EDGE_LOOP('',(#11912));
#2971=EDGE_LOOP('',(#11913,#11914,#11915,#11916));
#2972=EDGE_LOOP('',(#11917,#11918,#11919,#11920));
#2973=EDGE_LOOP('',(#11921,#11922,#11923,#11924));
#2974=EDGE_LOOP('',(#11925,#11926,#11927,#11928));
#2975=EDGE_LOOP('',(#11929,#11930,#11931,#11932));
#2976=EDGE_LOOP('',(#11933,#11934,#11935,#11936,#11937,#11938));
#2977=EDGE_LOOP('',(#11939,#11940,#11941,#11942));
#2978=EDGE_LOOP('',(#11943,#11944,#11945,#11946));
#3409=LINE('',#42290,#3857);
#3410=LINE('',#42293,#3858);
#3411=LINE('',#42296,#3859);
#3412=LINE('',#42301,#3860);
#3413=LINE('',#42304,#3861);
#3414=LINE('',#42368,#3862);
#3415=LINE('',#42372,#3863);
#3416=LINE('',#42377,#3864);
#3417=LINE('',#42383,#3865);
#3418=LINE('',#42387,#3866);
#3419=LINE('',#42392,#3867);
#3420=LINE('',#42398,#3868);
#3421=LINE('',#42406,#3869);
#3422=LINE('',#42409,#3870);
#3857=VECTOR('',#18117,8.14999999999999);
#3858=VECTOR('',#18122,7.5);
#3859=VECTOR('',#18125,7.5);
#3860=VECTOR('',#18132,12.4653846153846);
#3861=VECTOR('',#18135,12.4653846153846);
#3862=VECTOR('',#18210,17.6897435897436);
#3863=VECTOR('',#18215,16.2686153846154);
#3864=VECTOR('',#18222,16.0346153846154);
#3865=VECTOR('',#18231,16.0346153846154);
#3866=VECTOR('',#18236,16.2686153846154);
#3867=VECTOR('',#18241,17.6897435897436);
#3868=VECTOR('',#18248,20.35);
#3869=VECTOR('',#18257,21.);
#3870=VECTOR('',#18262,21.);
#4720=CIRCLE('',#14568,12.4653846153846);
#4721=CIRCLE('',#14569,3.56616156686793);
#4722=CIRCLE('',#14570,12.4653846153846);
#4723=CIRCLE('',#14572,7.64278544417155);
#4724=CIRCLE('',#14573,0.4875);
#4725=CIRCLE('',#14574,7.5);
#4726=CIRCLE('',#14575,7.5);
#4727=CIRCLE('',#14576,7.64278544417155);
#4728=CIRCLE('',#14578,7.5);
#4729=CIRCLE('',#14579,0.4875);
#4730=CIRCLE('',#14580,7.64278544417155);
#4731=CIRCLE('',#14581,7.5);
#4732=CIRCLE('',#14583,8.14999999999999);
#4733=CIRCLE('',#14586,8.14999999999999);
#4734=CIRCLE('',#14588,12.4653846153846);
#4735=CIRCLE('',#14590,12.4653846153846);
#4736=CIRCLE('',#14594,3.56616156686793);
#4737=CIRCLE('',#14596,3.56616156686793);
#4738=CIRCLE('',#14598,3.56616156686793);
#4739=CIRCLE('',#14600,3.56616156686793);
#4740=CIRCLE('',#14602,3.56616156686793);
#4741=CIRCLE('',#14604,3.56616156686793);
#4742=CIRCLE('',#14606,3.56616156686793);
#4743=CIRCLE('',#14608,16.3271153846154);
#4744=CIRCLE('',#14609,0.0585);
#4745=CIRCLE('',#14610,16.2686153846154);
#4746=CIRCLE('',#14611,16.2686153846154);
#4747=CIRCLE('',#14613,16.0346153846154);
#4748=CIRCLE('',#14614,0.0585);
#4749=CIRCLE('',#14615,16.0931153846154);
#4750=CIRCLE('',#14617,16.3271153846154);
#4751=CIRCLE('',#14618,0.0585);
#4752=CIRCLE('',#14619,16.2686153846154);
#4753=CIRCLE('',#14621,16.0346153846154);
#4754=CIRCLE('',#14622,0.0585);
#4755=CIRCLE('',#14623,16.0931153846154);
#4756=CIRCLE('',#14624,16.0346153846154);
#4757=CIRCLE('',#14626,17.6897435897436);
#4758=CIRCLE('',#14627,17.6897435897436);
#4759=CIRCLE('',#14629,16.2686153846154);
#4760=CIRCLE('',#14631,16.0346153846154);
#4761=CIRCLE('',#14633,3.56616156686793);
#4762=CIRCLE('',#14634,16.0346153846154);
#4763=CIRCLE('',#14637,16.2686153846154);
#4764=CIRCLE('',#14639,17.6897435897436);
#4765=CIRCLE('',#14640,17.6897435897436);
#4766=CIRCLE('',#14642,21.);
#4767=CIRCLE('',#14643,20.35);
#4768=CIRCLE('',#14645,21.);
#4769=CIRCLE('',#14646,21.);
#4770=CIRCLE('',#14647,20.35);
#4771=CIRCLE('',#14656,3.96060240207311);
#4772=CIRCLE('',#14657,1.69469015025);
#4773=CIRCLE('',#14658,3.96060240207311);
#4774=CIRCLE('',#14660,3.39763111739558);
#4775=CIRCLE('',#14661,3.39763111739558);
#4776=CIRCLE('',#14662,3.39763111739558);
#4777=CIRCLE('',#14663,3.56616156686792);
#4778=CIRCLE('',#14664,3.39763111739558);
#4779=CIRCLE('',#14665,3.39763111739558);
#4780=CIRCLE('',#14666,3.39763111739558);
#4781=CIRCLE('',#14667,3.45272288248773);
#4782=CIRCLE('',#14668,3.45272288248773);
#4783=CIRCLE('',#14670,3.96060240207311);
#4784=CIRCLE('',#14671,1.69469015025);
#4785=CIRCLE('',#14672,3.96060240207311);
#4786=CIRCLE('',#14674,3.39763111739558);
#4787=CIRCLE('',#14675,3.39763111739558);
#4788=CIRCLE('',#14676,3.39763111739558);
#4789=CIRCLE('',#14677,3.56616156686792);
#4790=CIRCLE('',#14678,3.39763111739558);
#4791=CIRCLE('',#14679,3.39763111739558);
#4792=CIRCLE('',#14680,3.39763111739558);
#4793=CIRCLE('',#14681,3.45272288248773);
#4794=CIRCLE('',#14682,3.45272288248773);
#4795=CIRCLE('',#14684,3.96060240207311);
#4796=CIRCLE('',#14685,1.69469015025);
#4797=CIRCLE('',#14686,3.96060240207311);
#4798=CIRCLE('',#14688,3.39763111739558);
#4799=CIRCLE('',#14689,3.39763111739558);
#4800=CIRCLE('',#14690,3.39763111739558);
#4801=CIRCLE('',#14691,3.56616156686792);
#4802=CIRCLE('',#14692,3.39763111739558);
#4803=CIRCLE('',#14693,3.39763111739558);
#4804=CIRCLE('',#14694,3.39763111739558);
#4805=CIRCLE('',#14695,3.45272288248773);
#4806=CIRCLE('',#14696,3.45272288248773);
#4807=CIRCLE('',#14698,3.96060240207311);
#4808=CIRCLE('',#14699,1.69469015025);
#4809=CIRCLE('',#14700,3.96060240207311);
#4810=CIRCLE('',#14702,3.39763111739558);
#4811=CIRCLE('',#14703,3.39763111739558);
#4812=CIRCLE('',#14704,3.39763111739558);
#4813=CIRCLE('',#14705,3.56616156686792);
#4814=CIRCLE('',#14706,3.39763111739558);
#4815=CIRCLE('',#14707,3.39763111739558);
#4816=CIRCLE('',#14708,3.39763111739558);
#4817=CIRCLE('',#14709,3.45272288248773);
#4818=CIRCLE('',#14710,3.45272288248773);
#4819=CIRCLE('',#14712,3.96060240207311);
#4820=CIRCLE('',#14713,1.69469015025);
#4821=CIRCLE('',#14714,3.96060240207311);
#4822=CIRCLE('',#14716,3.39763111739558);
#4823=CIRCLE('',#14717,3.39763111739558);
#4824=CIRCLE('',#14718,3.39763111739558);
#4825=CIRCLE('',#14719,3.56616156686792);
#4826=CIRCLE('',#14720,3.39763111739558);
#4827=CIRCLE('',#14721,3.39763111739558);
#4828=CIRCLE('',#14722,3.39763111739558);
#4829=CIRCLE('',#14723,3.45272288248773);
#4830=CIRCLE('',#14724,3.45272288248773);
#4831=CIRCLE('',#14726,3.96060240207311);
#4832=CIRCLE('',#14727,1.69469015025);
#4833=CIRCLE('',#14728,3.96060240207311);
#4834=CIRCLE('',#14730,3.39763111739558);
#4835=CIRCLE('',#14731,3.56616156686792);
#4836=CIRCLE('',#14732,3.39763111739558);
#4837=CIRCLE('',#14733,3.39763111739558);
#4838=CIRCLE('',#14734,3.39763111739558);
#4839=CIRCLE('',#14735,3.39763111739558);
#4840=CIRCLE('',#14736,3.39763111739558);
#4841=CIRCLE('',#14737,3.45272288248773);
#4842=CIRCLE('',#14738,3.45272288248773);
#4843=CIRCLE('',#14740,3.39763111739558);
#4844=CIRCLE('',#14741,3.39763111739558);
#4845=CIRCLE('',#14742,3.39763111739558);
#4846=CIRCLE('',#14743,3.56616156686792);
#4847=CIRCLE('',#14744,3.39763111739558);
#4848=CIRCLE('',#14745,3.39763111739558);
#4849=CIRCLE('',#14746,3.39763111739558);
#4850=CIRCLE('',#14747,3.45272288248773);
#4851=CIRCLE('',#14748,3.45272288248773);
#4852=CIRCLE('',#14750,3.96060240207311);
#4853=CIRCLE('',#14751,1.69469015025);
#4854=CIRCLE('',#14752,3.96060240207311);
#4855=CIRCLE('',#14754,14.25);
#4856=CIRCLE('',#14755,14.25);
#4857=CIRCLE('',#14757,15.1423076923077);
#4858=CIRCLE('',#14758,15.1423076923077);
#4859=CIRCLE('',#14764,14.25);
#4860=CIRCLE('',#14765,15.1423076923077);
#4861=CIRCLE('',#14767,15.1423076923077);
#4862=CIRCLE('',#14768,14.25);
#4863=CIRCLE('',#14774,15.1423076923077);
#4864=CIRCLE('',#14775,14.25);
#4865=CIRCLE('',#14777,14.25);
#4866=CIRCLE('',#14778,15.1423076923077);
#4867=CIRCLE('',#14782,14.25);
#4868=CIRCLE('',#14783,14.25);
#4869=CIRCLE('',#14785,15.1423076923077);
#4870=CIRCLE('',#14786,15.1423076923077);
#4871=CIRCLE('',#14792,15.1423076923077);
#4872=CIRCLE('',#14793,14.25);
#4873=CIRCLE('',#14795,14.25);
#4874=CIRCLE('',#14796,15.1423076923077);
#4875=CIRCLE('',#14800,14.25);
#4876=CIRCLE('',#14801,14.25);
#4877=CIRCLE('',#14803,15.1423076923077);
#4878=CIRCLE('',#14804,15.1423076923077);
#4879=CIRCLE('',#14810,15.1423076923077);
#4880=CIRCLE('',#14811,14.25);
#4881=CIRCLE('',#14813,14.25);
#4882=CIRCLE('',#14814,15.1423076923077);
#4883=CIRCLE('',#14818,14.25);
#4884=CIRCLE('',#14819,14.25);
#4885=CIRCLE('',#14821,15.1423076923077);
#4886=CIRCLE('',#14822,15.1423076923077);
#4887=CIRCLE('',#14828,15.1423076923077);
#4888=CIRCLE('',#14829,14.25);
#4889=CIRCLE('',#14831,14.25);
#4890=CIRCLE('',#14832,15.1423076923077);
#4891=CIRCLE('',#14836,14.25);
#4892=CIRCLE('',#14837,14.25);
#4893=CIRCLE('',#14839,15.1423076923077);
#4894=CIRCLE('',#14840,15.1423076923077);
#4895=CIRCLE('',#14846,15.1423076923077);
#4896=CIRCLE('',#14847,14.25);
#4897=CIRCLE('',#14849,14.25);
#4898=CIRCLE('',#14850,15.1423076923077);
#4899=CIRCLE('',#14854,14.25);
#4900=CIRCLE('',#14855,14.25);
#4901=CIRCLE('',#14857,15.1423076923077);
#4902=CIRCLE('',#14858,15.1423076923077);
#4903=CIRCLE('',#14864,15.1423076923077);
#4904=CIRCLE('',#14865,14.25);
#4905=CIRCLE('',#14867,14.25);
#4906=CIRCLE('',#14868,15.1423076923077);
#4907=CIRCLE('',#14872,15.1423076923077);
#4908=CIRCLE('',#14873,14.25);
#4909=CIRCLE('',#14875,14.25);
#4910=CIRCLE('',#14876,15.1423076923077);
#6019=VERTEX_POINT('',#42265);
#6020=VERTEX_POINT('',#42267);
#6021=VERTEX_POINT('',#42271);
#6022=VERTEX_POINT('',#42272);
#6023=VERTEX_POINT('',#42274);
#6024=VERTEX_POINT('',#42276);
#6025=VERTEX_POINT('',#42281);
#6026=VERTEX_POINT('',#42282);
#6027=VERTEX_POINT('',#42284);
#6028=VERTEX_POINT('',#42289);
#6029=VERTEX_POINT('',#42295);
#6030=VERTEX_POINT('',#42299);
#6031=VERTEX_POINT('',#42303);
#6032=VERTEX_POINT('',#42309);
#6033=VERTEX_POINT('',#42310);
#6034=VERTEX_POINT('',#42313);
#6035=VERTEX_POINT('',#42314);
#6036=VERTEX_POINT('',#42317);
#6037=VERTEX_POINT('',#42318);
#6038=VERTEX_POINT('',#42321);
#6039=VERTEX_POINT('',#42322);
#6040=VERTEX_POINT('',#42325);
#6041=VERTEX_POINT('',#42326);
#6042=VERTEX_POINT('',#42329);
#6043=VERTEX_POINT('',#42330);
#6044=VERTEX_POINT('',#42333);
#6045=VERTEX_POINT('',#42334);
#6046=VERTEX_POINT('',#42337);
#6047=VERTEX_POINT('',#42339);
#6048=VERTEX_POINT('',#42341);
#6049=VERTEX_POINT('',#42345);
#6050=VERTEX_POINT('',#42347);
#6051=VERTEX_POINT('',#42351);
#6052=VERTEX_POINT('',#42353);
#6053=VERTEX_POINT('',#42357);
#6054=VERTEX_POINT('',#42358);
#6055=VERTEX_POINT('',#42360);
#6056=VERTEX_POINT('',#42365);
#6057=VERTEX_POINT('',#42367);
#6058=VERTEX_POINT('',#42371);
#6059=VERTEX_POINT('',#42375);
#6060=VERTEX_POINT('',#42379);
#6061=VERTEX_POINT('',#42385);
#6062=VERTEX_POINT('',#42389);
#6063=VERTEX_POINT('',#42391);
#6064=VERTEX_POINT('',#42395);
#6065=VERTEX_POINT('',#42397);
#6066=VERTEX_POINT('',#42401);
#6067=VERTEX_POINT('',#42402);
#6068=VERTEX_POINT('',#42405);
#6069=VERTEX_POINT('',#42417);
#6070=VERTEX_POINT('',#42419);
#6071=VERTEX_POINT('',#42422);
#6072=VERTEX_POINT('',#42423);
#6073=VERTEX_POINT('',#42430);
#6074=VERTEX_POINT('',#42450);
#6075=VERTEX_POINT('',#42476);
#6076=VERTEX_POINT('',#42477);
#6077=VERTEX_POINT('',#42484);
#6078=VERTEX_POINT('',#42504);
#6079=VERTEX_POINT('',#42531);
#6080=VERTEX_POINT('',#42532);
#6081=VERTEX_POINT('',#42534);
#6082=VERTEX_POINT('',#42541);
#6083=VERTEX_POINT('',#42543);
#6084=VERTEX_POINT('',#42551);
#6085=VERTEX_POINT('',#42553);
#6086=VERTEX_POINT('',#42555);
#6087=VERTEX_POINT('',#42563);
#6088=VERTEX_POINT('',#42565);
#6089=VERTEX_POINT('',#42574);
#6090=VERTEX_POINT('',#42576);
#6091=VERTEX_POINT('',#42579);
#6092=VERTEX_POINT('',#42581);
#6093=VERTEX_POINT('',#42584);
#6094=VERTEX_POINT('',#42585);
#6095=VERTEX_POINT('',#42592);
#6096=VERTEX_POINT('',#42612);
#6097=VERTEX_POINT('',#42638);
#6098=VERTEX_POINT('',#42639);
#6099=VERTEX_POINT('',#42646);
#6100=VERTEX_POINT('',#42666);
#6101=VERTEX_POINT('',#42693);
#6102=VERTEX_POINT('',#42694);
#6103=VERTEX_POINT('',#42696);
#6104=VERTEX_POINT('',#42703);
#6105=VERTEX_POINT('',#42705);
#6106=VERTEX_POINT('',#42713);
#6107=VERTEX_POINT('',#42715);
#6108=VERTEX_POINT('',#42717);
#6109=VERTEX_POINT('',#42725);
#6110=VERTEX_POINT('',#42727);
#6111=VERTEX_POINT('',#42736);
#6112=VERTEX_POINT('',#42738);
#6113=VERTEX_POINT('',#42741);
#6114=VERTEX_POINT('',#42743);
#6115=VERTEX_POINT('',#42746);
#6116=VERTEX_POINT('',#42747);
#6117=VERTEX_POINT('',#42754);
#6118=VERTEX_POINT('',#42774);
#6119=VERTEX_POINT('',#42800);
#6120=VERTEX_POINT('',#42801);
#6121=VERTEX_POINT('',#42808);
#6122=VERTEX_POINT('',#42828);
#6123=VERTEX_POINT('',#42855);
#6124=VERTEX_POINT('',#42856);
#6125=VERTEX_POINT('',#42858);
#6126=VERTEX_POINT('',#42865);
#6127=VERTEX_POINT('',#42867);
#6128=VERTEX_POINT('',#42875);
#6129=VERTEX_POINT('',#42877);
#6130=VERTEX_POINT('',#42879);
#6131=VERTEX_POINT('',#42887);
#6132=VERTEX_POINT('',#42889);
#6133=VERTEX_POINT('',#42898);
#6134=VERTEX_POINT('',#42900);
#6135=VERTEX_POINT('',#42903);
#6136=VERTEX_POINT('',#42905);
#6137=VERTEX_POINT('',#42908);
#6138=VERTEX_POINT('',#42909);
#6139=VERTEX_POINT('',#42916);
#6140=VERTEX_POINT('',#42936);
#6141=VERTEX_POINT('',#42962);
#6142=VERTEX_POINT('',#42963);
#6143=VERTEX_POINT('',#42970);
#6144=VERTEX_POINT('',#42990);
#6145=VERTEX_POINT('',#43017);
#6146=VERTEX_POINT('',#43018);
#6147=VERTEX_POINT('',#43020);
#6148=VERTEX_POINT('',#43027);
#6149=VERTEX_POINT('',#43029);
#6150=VERTEX_POINT('',#43037);
#6151=VERTEX_POINT('',#43039);
#6152=VERTEX_POINT('',#43041);
#6153=VERTEX_POINT('',#43049);
#6154=VERTEX_POINT('',#43051);
#6155=VERTEX_POINT('',#43060);
#6156=VERTEX_POINT('',#43062);
#6157=VERTEX_POINT('',#43065);
#6158=VERTEX_POINT('',#43067);
#6159=VERTEX_POINT('',#43070);
#6160=VERTEX_POINT('',#43071);
#6161=VERTEX_POINT('',#43078);
#6162=VERTEX_POINT('',#43098);
#6163=VERTEX_POINT('',#43124);
#6164=VERTEX_POINT('',#43125);
#6165=VERTEX_POINT('',#43132);
#6166=VERTEX_POINT('',#43152);
#6167=VERTEX_POINT('',#43179);
#6168=VERTEX_POINT('',#43180);
#6169=VERTEX_POINT('',#43182);
#6170=VERTEX_POINT('',#43189);
#6171=VERTEX_POINT('',#43191);
#6172=VERTEX_POINT('',#43199);
#6173=VERTEX_POINT('',#43201);
#6174=VERTEX_POINT('',#43203);
#6175=VERTEX_POINT('',#43211);
#6176=VERTEX_POINT('',#43213);
#6177=VERTEX_POINT('',#43222);
#6178=VERTEX_POINT('',#43224);
#6179=VERTEX_POINT('',#43227);
#6180=VERTEX_POINT('',#43229);
#6181=VERTEX_POINT('',#43232);
#6182=VERTEX_POINT('',#43233);
#6183=VERTEX_POINT('',#43253);
#6184=VERTEX_POINT('',#43260);
#6185=VERTEX_POINT('',#43286);
#6186=VERTEX_POINT('',#43287);
#6187=VERTEX_POINT('',#43294);
#6188=VERTEX_POINT('',#43314);
#6189=VERTEX_POINT('',#43341);
#6190=VERTEX_POINT('',#43342);
#6191=VERTEX_POINT('',#43344);
#6192=VERTEX_POINT('',#43346);
#6193=VERTEX_POINT('',#43348);
#6194=VERTEX_POINT('',#43356);
#6195=VERTEX_POINT('',#43358);
#6196=VERTEX_POINT('',#43367);
#6197=VERTEX_POINT('',#43369);
#6198=VERTEX_POINT('',#43376);
#6199=VERTEX_POINT('',#43384);
#6200=VERTEX_POINT('',#43386);
#6201=VERTEX_POINT('',#43389);
#6202=VERTEX_POINT('',#43390);
#6203=VERTEX_POINT('',#43392);
#6204=VERTEX_POINT('',#43399);
#6205=VERTEX_POINT('',#43401);
#6206=VERTEX_POINT('',#43409);
#6207=VERTEX_POINT('',#43411);
#6208=VERTEX_POINT('',#43413);
#6209=VERTEX_POINT('',#43421);
#6210=VERTEX_POINT('',#43423);
#6211=VERTEX_POINT('',#43432);
#6212=VERTEX_POINT('',#43434);
#6213=VERTEX_POINT('',#43437);
#6214=VERTEX_POINT('',#43439);
#6215=VERTEX_POINT('',#43442);
#6216=VERTEX_POINT('',#43443);
#6217=VERTEX_POINT('',#43450);
#6218=VERTEX_POINT('',#43470);
#6219=VERTEX_POINT('',#43496);
#6220=VERTEX_POINT('',#43497);
#6221=VERTEX_POINT('',#43504);
#6222=VERTEX_POINT('',#43524);
#7846=EDGE_CURVE('',#6019,#6019,#4720,.T.);
#7847=EDGE_CURVE('',#6019,#6020,#4721,.T.);
#7848=EDGE_CURVE('',#6020,#6020,#4722,.T.);
#7849=EDGE_CURVE('',#6021,#6022,#4723,.T.);
#7850=EDGE_CURVE('',#6022,#6023,#4724,.T.);
#7851=EDGE_CURVE('',#6023,#6024,#4725,.T.);
#7852=EDGE_CURVE('',#6024,#6023,#4726,.T.);
#7853=EDGE_CURVE('',#6022,#6021,#4727,.T.);
#7854=EDGE_CURVE('',#6025,#6026,#4728,.T.);
#7855=EDGE_CURVE('',#6026,#6027,#4729,.T.);
#7856=EDGE_CURVE('',#6027,#6027,#4730,.T.);
#7857=EDGE_CURVE('',#6026,#6025,#4731,.T.);
#7858=EDGE_CURVE('',#6021,#6028,#3409,.T.);
#7859=EDGE_CURVE('',#6028,#6028,#4732,.T.);
#7860=EDGE_CURVE('',#6024,#6025,#3410,.T.);
#7861=EDGE_CURVE('',#6027,#6029,#3411,.T.);
#7862=EDGE_CURVE('',#6029,#6029,#4733,.T.);
#7863=EDGE_CURVE('',#6030,#6030,#4734,.T.);
#7864=EDGE_CURVE('',#6030,#6020,#3412,.T.);
#7865=EDGE_CURVE('',#6019,#6031,#3413,.T.);
#7866=EDGE_CURVE('',#6031,#6031,#4735,.T.);
#7867=EDGE_CURVE('',#6032,#6033,#4736,.T.);
#7868=EDGE_CURVE('',#6034,#6035,#4737,.T.);
#7869=EDGE_CURVE('',#6036,#6037,#4738,.T.);
#7870=EDGE_CURVE('',#6038,#6039,#4739,.T.);
#7871=EDGE_CURVE('',#6040,#6041,#4740,.T.);
#7872=EDGE_CURVE('',#6042,#6043,#4741,.T.);
#7873=EDGE_CURVE('',#6044,#6045,#4742,.T.);
#7874=EDGE_CURVE('',#6046,#6046,#4743,.T.);
#7875=EDGE_CURVE('',#6046,#6047,#4744,.T.);
#7876=EDGE_CURVE('',#6047,#6048,#4745,.T.);
#7877=EDGE_CURVE('',#6048,#6047,#4746,.T.);
#7878=EDGE_CURVE('',#6049,#6049,#4747,.T.);
#7879=EDGE_CURVE('',#6049,#6050,#4748,.T.);
#7880=EDGE_CURVE('',#6050,#6050,#4749,.T.);
#7881=EDGE_CURVE('',#6051,#6051,#4750,.T.);
#7882=EDGE_CURVE('',#6051,#6052,#4751,.T.);
#7883=EDGE_CURVE('',#6052,#6052,#4752,.T.);
#7884=EDGE_CURVE('',#6053,#6054,#4753,.T.);
#7885=EDGE_CURVE('',#6054,#6055,#4754,.T.);
#7886=EDGE_CURVE('',#6055,#6055,#4755,.T.);
#7887=EDGE_CURVE('',#6054,#6053,#4756,.T.);
#7888=EDGE_CURVE('',#6056,#6056,#4757,.T.);
#7889=EDGE_CURVE('',#6056,#6057,#3414,.T.);
#7890=EDGE_CURVE('',#6057,#6057,#4758,.T.);
#7891=EDGE_CURVE('',#6048,#6058,#3415,.T.);
#7892=EDGE_CURVE('',#6058,#6058,#4759,.T.);
#7893=EDGE_CURVE('',#6059,#6059,#4760,.T.);
#7894=EDGE_CURVE('',#6059,#6053,#3416,.T.);
#7895=EDGE_CURVE('',#6059,#6060,#4761,.T.);
#7896=EDGE_CURVE('',#6060,#6060,#4762,.T.);
#7897=EDGE_CURVE('',#6049,#6060,#3417,.T.);
#7898=EDGE_CURVE('',#6061,#6061,#4763,.T.);
#7899=EDGE_CURVE('',#6061,#6052,#3418,.T.);
#7900=EDGE_CURVE('',#6062,#6062,#4764,.T.);
#7901=EDGE_CURVE('',#6062,#6063,#3419,.T.);
#7902=EDGE_CURVE('',#6063,#6063,#4765,.T.);
#7903=EDGE_CURVE('',#6064,#6064,#4766,.T.);
#7904=EDGE_CURVE('',#6064,#6065,#3420,.T.);
#7905=EDGE_CURVE('',#6065,#6065,#4767,.T.);
#7906=EDGE_CURVE('',#6066,#6067,#4768,.T.);
#7907=EDGE_CURVE('',#6067,#6066,#4769,.T.);
#7908=EDGE_CURVE('',#6067,#6068,#3421,.T.);
#7909=EDGE_CURVE('',#6068,#6068,#4770,.T.);
#7910=EDGE_CURVE('',#6064,#6066,#3422,.T.);
#7911=EDGE_CURVE('',#6069,#6069,#4771,.T.);
#7912=EDGE_CURVE('',#6069,#6070,#4772,.T.);
#7913=EDGE_CURVE('',#6070,#6070,#4773,.T.);
#7914=EDGE_CURVE('',#6071,#6072,#863,.T.);
#7915=EDGE_CURVE('',#6073,#6072,#864,.T.);
#7916=EDGE_CURVE('',#6074,#6073,#865,.T.);
#7917=EDGE_CURVE('',#6071,#6074,#866,.T.);
#7918=EDGE_CURVE('',#6075,#6076,#867,.T.);
#7919=EDGE_CURVE('',#6077,#6076,#868,.T.);
#7920=EDGE_CURVE('',#6078,#6077,#869,.T.);
#7921=EDGE_CURVE('',#6075,#6078,#870,.T.);
#7922=EDGE_CURVE('',#6079,#6080,#4774,.T.);
#7923=EDGE_CURVE('',#6081,#6079,#871,.T.);
#7924=EDGE_CURVE('',#6081,#6082,#4775,.T.);
#7925=EDGE_CURVE('',#6083,#6082,#872,.T.);
#7926=EDGE_CURVE('',#6080,#6083,#4776,.T.);
#7927=EDGE_CURVE('',#6080,#6084,#4777,.T.);
#7928=EDGE_CURVE('',#6085,#6084,#4778,.T.);
#7929=EDGE_CURVE('',#6086,#6085,#873,.T.);
#7930=EDGE_CURVE('',#6086,#6087,#4779,.T.);
#7931=EDGE_CURVE('',#6088,#6087,#874,.T.);
#7932=EDGE_CURVE('',#6084,#6088,#4780,.T.);
#7933=EDGE_CURVE('',#6089,#6089,#4781,.T.);
#7934=EDGE_CURVE('',#6090,#6090,#4782,.T.);
#7935=EDGE_CURVE('',#6091,#6091,#4783,.T.);
#7936=EDGE_CURVE('',#6091,#6092,#4784,.T.);
#7937=EDGE_CURVE('',#6092,#6092,#4785,.T.);
#7938=EDGE_CURVE('',#6093,#6094,#875,.T.);
#7939=EDGE_CURVE('',#6095,#6094,#876,.T.);
#7940=EDGE_CURVE('',#6096,#6095,#877,.T.);
#7941=EDGE_CURVE('',#6093,#6096,#878,.T.);
#7942=EDGE_CURVE('',#6097,#6098,#879,.T.);
#7943=EDGE_CURVE('',#6099,#6098,#880,.T.);
#7944=EDGE_CURVE('',#6100,#6099,#881,.T.);
#7945=EDGE_CURVE('',#6097,#6100,#882,.T.);
#7946=EDGE_CURVE('',#6101,#6102,#4786,.T.);
#7947=EDGE_CURVE('',#6103,#6101,#883,.T.);
#7948=EDGE_CURVE('',#6103,#6104,#4787,.T.);
#7949=EDGE_CURVE('',#6105,#6104,#884,.T.);
#7950=EDGE_CURVE('',#6102,#6105,#4788,.T.);
#7951=EDGE_CURVE('',#6102,#6106,#4789,.T.);
#7952=EDGE_CURVE('',#6107,#6106,#4790,.T.);
#7953=EDGE_CURVE('',#6108,#6107,#885,.T.);
#7954=EDGE_CURVE('',#6108,#6109,#4791,.T.);
#7955=EDGE_CURVE('',#6110,#6109,#886,.T.);
#7956=EDGE_CURVE('',#6106,#6110,#4792,.T.);
#7957=EDGE_CURVE('',#6111,#6111,#4793,.T.);
#7958=EDGE_CURVE('',#6112,#6112,#4794,.T.);
#7959=EDGE_CURVE('',#6113,#6113,#4795,.T.);
#7960=EDGE_CURVE('',#6113,#6114,#4796,.T.);
#7961=EDGE_CURVE('',#6114,#6114,#4797,.T.);
#7962=EDGE_CURVE('',#6115,#6116,#887,.T.);
#7963=EDGE_CURVE('',#6117,#6116,#888,.T.);
#7964=EDGE_CURVE('',#6118,#6117,#889,.T.);
#7965=EDGE_CURVE('',#6115,#6118,#890,.T.);
#7966=EDGE_CURVE('',#6119,#6120,#891,.T.);
#7967=EDGE_CURVE('',#6121,#6120,#892,.T.);
#7968=EDGE_CURVE('',#6122,#6121,#893,.T.);
#7969=EDGE_CURVE('',#6119,#6122,#894,.T.);
#7970=EDGE_CURVE('',#6123,#6124,#4798,.T.);
#7971=EDGE_CURVE('',#6125,#6123,#895,.T.);
#7972=EDGE_CURVE('',#6125,#6126,#4799,.T.);
#7973=EDGE_CURVE('',#6127,#6126,#896,.T.);
#7974=EDGE_CURVE('',#6124,#6127,#4800,.T.);
#7975=EDGE_CURVE('',#6124,#6128,#4801,.T.);
#7976=EDGE_CURVE('',#6129,#6128,#4802,.T.);
#7977=EDGE_CURVE('',#6130,#6129,#897,.T.);
#7978=EDGE_CURVE('',#6130,#6131,#4803,.T.);
#7979=EDGE_CURVE('',#6132,#6131,#898,.T.);
#7980=EDGE_CURVE('',#6128,#6132,#4804,.T.);
#7981=EDGE_CURVE('',#6133,#6133,#4805,.T.);
#7982=EDGE_CURVE('',#6134,#6134,#4806,.T.);
#7983=EDGE_CURVE('',#6135,#6135,#4807,.T.);
#7984=EDGE_CURVE('',#6135,#6136,#4808,.T.);
#7985=EDGE_CURVE('',#6136,#6136,#4809,.T.);
#7986=EDGE_CURVE('',#6137,#6138,#899,.T.);
#7987=EDGE_CURVE('',#6139,#6138,#900,.T.);
#7988=EDGE_CURVE('',#6140,#6139,#901,.T.);
#7989=EDGE_CURVE('',#6137,#6140,#902,.T.);
#7990=EDGE_CURVE('',#6141,#6142,#903,.T.);
#7991=EDGE_CURVE('',#6143,#6142,#904,.T.);
#7992=EDGE_CURVE('',#6144,#6143,#905,.T.);
#7993=EDGE_CURVE('',#6141,#6144,#906,.T.);
#7994=EDGE_CURVE('',#6145,#6146,#4810,.T.);
#7995=EDGE_CURVE('',#6147,#6145,#907,.T.);
#7996=EDGE_CURVE('',#6147,#6148,#4811,.T.);
#7997=EDGE_CURVE('',#6149,#6148,#908,.T.);
#7998=EDGE_CURVE('',#6146,#6149,#4812,.T.);
#7999=EDGE_CURVE('',#6146,#6150,#4813,.T.);
#8000=EDGE_CURVE('',#6151,#6150,#4814,.T.);
#8001=EDGE_CURVE('',#6152,#6151,#909,.T.);
#8002=EDGE_CURVE('',#6152,#6153,#4815,.T.);
#8003=EDGE_CURVE('',#6154,#6153,#910,.T.);
#8004=EDGE_CURVE('',#6150,#6154,#4816,.T.);
#8005=EDGE_CURVE('',#6155,#6155,#4817,.T.);
#8006=EDGE_CURVE('',#6156,#6156,#4818,.T.);
#8007=EDGE_CURVE('',#6157,#6157,#4819,.T.);
#8008=EDGE_CURVE('',#6157,#6158,#4820,.T.);
#8009=EDGE_CURVE('',#6158,#6158,#4821,.T.);
#8010=EDGE_CURVE('',#6159,#6160,#911,.T.);
#8011=EDGE_CURVE('',#6161,#6160,#912,.T.);
#8012=EDGE_CURVE('',#6162,#6161,#913,.T.);
#8013=EDGE_CURVE('',#6159,#6162,#914,.T.);
#8014=EDGE_CURVE('',#6163,#6164,#915,.T.);
#8015=EDGE_CURVE('',#6165,#6164,#916,.T.);
#8016=EDGE_CURVE('',#6166,#6165,#917,.T.);
#8017=EDGE_CURVE('',#6163,#6166,#918,.T.);
#8018=EDGE_CURVE('',#6167,#6168,#4822,.T.);
#8019=EDGE_CURVE('',#6169,#6167,#919,.T.);
#8020=EDGE_CURVE('',#6169,#6170,#4823,.T.);
#8021=EDGE_CURVE('',#6171,#6170,#920,.T.);
#8022=EDGE_CURVE('',#6168,#6171,#4824,.T.);
#8023=EDGE_CURVE('',#6168,#6172,#4825,.T.);
#8024=EDGE_CURVE('',#6173,#6172,#4826,.T.);
#8025=EDGE_CURVE('',#6174,#6173,#921,.T.);
#8026=EDGE_CURVE('',#6174,#6175,#4827,.T.);
#8027=EDGE_CURVE('',#6176,#6175,#922,.T.);
#8028=EDGE_CURVE('',#6172,#6176,#4828,.T.);
#8029=EDGE_CURVE('',#6177,#6177,#4829,.T.);
#8030=EDGE_CURVE('',#6178,#6178,#4830,.T.);
#8031=EDGE_CURVE('',#6179,#6179,#4831,.T.);
#8032=EDGE_CURVE('',#6179,#6180,#4832,.T.);
#8033=EDGE_CURVE('',#6180,#6180,#4833,.T.);
#8034=EDGE_CURVE('',#6181,#6182,#923,.T.);
#8035=EDGE_CURVE('',#6182,#6183,#924,.T.);
#8036=EDGE_CURVE('',#6183,#6184,#925,.T.);
#8037=EDGE_CURVE('',#6181,#6184,#926,.T.);
#8038=EDGE_CURVE('',#6185,#6186,#927,.T.);
#8039=EDGE_CURVE('',#6187,#6186,#928,.T.);
#8040=EDGE_CURVE('',#6188,#6187,#929,.T.);
#8041=EDGE_CURVE('',#6185,#6188,#930,.T.);
#8042=EDGE_CURVE('',#6189,#6190,#4834,.T.);
#8043=EDGE_CURVE('',#6190,#6191,#4835,.T.);
#8044=EDGE_CURVE('',#6192,#6191,#4836,.T.);
#8045=EDGE_CURVE('',#6193,#6192,#931,.T.);
#8046=EDGE_CURVE('',#6193,#6194,#4837,.T.);
#8047=EDGE_CURVE('',#6195,#6194,#932,.T.);
#8048=EDGE_CURVE('',#6191,#6195,#4838,.T.);
#8049=EDGE_CURVE('',#6190,#6196,#4839,.T.);
#8050=EDGE_CURVE('',#6196,#6197,#933,.T.);
#8051=EDGE_CURVE('',#6198,#6197,#4840,.T.);
#8052=EDGE_CURVE('',#6198,#6189,#934,.T.);
#8053=EDGE_CURVE('',#6199,#6199,#4841,.T.);
#8054=EDGE_CURVE('',#6200,#6200,#4842,.T.);
#8055=EDGE_CURVE('',#6201,#6202,#4843,.T.);
#8056=EDGE_CURVE('',#6203,#6201,#935,.T.);
#8057=EDGE_CURVE('',#6203,#6204,#4844,.T.);
#8058=EDGE_CURVE('',#6205,#6204,#936,.T.);
#8059=EDGE_CURVE('',#6202,#6205,#4845,.T.);
#8060=EDGE_CURVE('',#6202,#6206,#4846,.T.);
#8061=EDGE_CURVE('',#6207,#6206,#4847,.T.);
#8062=EDGE_CURVE('',#6208,#6207,#937,.T.);
#8063=EDGE_CURVE('',#6208,#6209,#4848,.T.);
#8064=EDGE_CURVE('',#6210,#6209,#938,.T.);
#8065=EDGE_CURVE('',#6206,#6210,#4849,.T.);
#8066=EDGE_CURVE('',#6211,#6211,#4850,.T.);
#8067=EDGE_CURVE('',#6212,#6212,#4851,.T.);
#8068=EDGE_CURVE('',#6213,#6213,#4852,.T.);
#8069=EDGE_CURVE('',#6213,#6214,#4853,.T.);
#8070=EDGE_CURVE('',#6214,#6214,#4854,.T.);
#8071=EDGE_CURVE('',#6215,#6216,#939,.T.);
#8072=EDGE_CURVE('',#6217,#6216,#940,.T.);
#8073=EDGE_CURVE('',#6218,#6217,#941,.T.);
#8074=EDGE_CURVE('',#6215,#6218,#942,.T.);
#8075=EDGE_CURVE('',#6219,#6220,#943,.T.);
#8076=EDGE_CURVE('',#6221,#6220,#944,.T.);
#8077=EDGE_CURVE('',#6222,#6221,#945,.T.);
#8078=EDGE_CURVE('',#6219,#6222,#946,.T.);
#8079=EDGE_CURVE('',#6221,#6183,#4855,.T.);
#8080=EDGE_CURVE('',#6220,#6184,#4856,.T.);
#8081=EDGE_CURVE('',#6181,#6219,#4857,.T.);
#8082=EDGE_CURVE('',#6182,#6222,#4858,.T.);
#8083=EDGE_CURVE('',#6204,#6208,#4859,.T.);
#8084=EDGE_CURVE('',#6209,#6203,#4860,.T.);
#8085=EDGE_CURVE('',#6210,#6201,#4861,.T.);
#8086=EDGE_CURVE('',#6205,#6207,#4862,.T.);
#8087=EDGE_CURVE('',#6161,#6188,#4863,.T.);
#8088=EDGE_CURVE('',#6187,#6162,#4864,.T.);
#8089=EDGE_CURVE('',#6186,#6159,#4865,.T.);
#8090=EDGE_CURVE('',#6160,#6185,#4866,.T.);
#8091=EDGE_CURVE('',#6171,#6173,#4867,.T.);
#8092=EDGE_CURVE('',#6170,#6174,#4868,.T.);
#8093=EDGE_CURVE('',#6175,#6169,#4869,.T.);
#8094=EDGE_CURVE('',#6176,#6167,#4870,.T.);
#8095=EDGE_CURVE('',#6139,#6166,#4871,.T.);
#8096=EDGE_CURVE('',#6165,#6140,#4872,.T.);
#8097=EDGE_CURVE('',#6164,#6137,#4873,.T.);
#8098=EDGE_CURVE('',#6138,#6163,#4874,.T.);
#8099=EDGE_CURVE('',#6149,#6151,#4875,.T.);
#8100=EDGE_CURVE('',#6148,#6152,#4876,.T.);
#8101=EDGE_CURVE('',#6153,#6147,#4877,.T.);
#8102=EDGE_CURVE('',#6154,#6145,#4878,.T.);
#8103=EDGE_CURVE('',#6117,#6144,#4879,.T.);
#8104=EDGE_CURVE('',#6143,#6118,#4880,.T.);
#8105=EDGE_CURVE('',#6142,#6115,#4881,.T.);
#8106=EDGE_CURVE('',#6116,#6141,#4882,.T.);
#8107=EDGE_CURVE('',#6127,#6129,#4883,.T.);
#8108=EDGE_CURVE('',#6126,#6130,#4884,.T.);
#8109=EDGE_CURVE('',#6131,#6125,#4885,.T.);
#8110=EDGE_CURVE('',#6132,#6123,#4886,.T.);
#8111=EDGE_CURVE('',#6095,#6122,#4887,.T.);
#8112=EDGE_CURVE('',#6121,#6096,#4888,.T.);
#8113=EDGE_CURVE('',#6120,#6093,#4889,.T.);
#8114=EDGE_CURVE('',#6094,#6119,#4890,.T.);
#8115=EDGE_CURVE('',#6105,#6107,#4891,.T.);
#8116=EDGE_CURVE('',#6104,#6108,#4892,.T.);
#8117=EDGE_CURVE('',#6109,#6103,#4893,.T.);
#8118=EDGE_CURVE('',#6110,#6101,#4894,.T.);
#8119=EDGE_CURVE('',#6073,#6100,#4895,.T.);
#8120=EDGE_CURVE('',#6099,#6074,#4896,.T.);
#8121=EDGE_CURVE('',#6098,#6071,#4897,.T.);
#8122=EDGE_CURVE('',#6072,#6097,#4898,.T.);
#8123=EDGE_CURVE('',#6083,#6085,#4899,.T.);
#8124=EDGE_CURVE('',#6082,#6086,#4900,.T.);
#8125=EDGE_CURVE('',#6087,#6081,#4901,.T.);
#8126=EDGE_CURVE('',#6088,#6079,#4902,.T.);
#8127=EDGE_CURVE('',#6217,#6078,#4903,.T.);
#8128=EDGE_CURVE('',#6077,#6218,#4904,.T.);
#8129=EDGE_CURVE('',#6076,#6215,#4905,.T.);
#8130=EDGE_CURVE('',#6216,#6075,#4906,.T.);
#8131=EDGE_CURVE('',#6194,#6197,#4907,.T.);
#8132=EDGE_CURVE('',#6198,#6193,#4908,.T.);
#8133=EDGE_CURVE('',#6189,#6192,#4909,.T.);
#8134=EDGE_CURVE('',#6195,#6196,#4910,.T.);
#11369=ORIENTED_EDGE('',*,*,#7846,.T.);
#11370=ORIENTED_EDGE('',*,*,#7847,.T.);
#11371=ORIENTED_EDGE('',*,*,#7848,.F.);
#11372=ORIENTED_EDGE('',*,*,#7847,.F.);
#11373=ORIENTED_EDGE('',*,*,#7849,.T.);
#11374=ORIENTED_EDGE('',*,*,#7850,.T.);
#11375=ORIENTED_EDGE('',*,*,#7851,.T.);
#11376=ORIENTED_EDGE('',*,*,#7852,.T.);
#11377=ORIENTED_EDGE('',*,*,#7850,.F.);
#11378=ORIENTED_EDGE('',*,*,#7853,.T.);
#11379=ORIENTED_EDGE('',*,*,#7854,.T.);
#11380=ORIENTED_EDGE('',*,*,#7855,.T.);
#11381=ORIENTED_EDGE('',*,*,#7856,.T.);
#11382=ORIENTED_EDGE('',*,*,#7855,.F.);
#11383=ORIENTED_EDGE('',*,*,#7857,.T.);
#11384=ORIENTED_EDGE('',*,*,#7849,.F.);
#11385=ORIENTED_EDGE('',*,*,#7858,.T.);
#11386=ORIENTED_EDGE('',*,*,#7859,.F.);
#11387=ORIENTED_EDGE('',*,*,#7858,.F.);
#11388=ORIENTED_EDGE('',*,*,#7853,.F.);
#11389=ORIENTED_EDGE('',*,*,#7852,.F.);
#11390=ORIENTED_EDGE('',*,*,#7860,.T.);
#11391=ORIENTED_EDGE('',*,*,#7857,.F.);
#11392=ORIENTED_EDGE('',*,*,#7854,.F.);
#11393=ORIENTED_EDGE('',*,*,#7860,.F.);
#11394=ORIENTED_EDGE('',*,*,#7851,.F.);
#11395=ORIENTED_EDGE('',*,*,#7856,.F.);
#11396=ORIENTED_EDGE('',*,*,#7861,.T.);
#11397=ORIENTED_EDGE('',*,*,#7862,.T.);
#11398=ORIENTED_EDGE('',*,*,#7861,.F.);
#11399=ORIENTED_EDGE('',*,*,#7863,.F.);
#11400=ORIENTED_EDGE('',*,*,#7864,.T.);
#11401=ORIENTED_EDGE('',*,*,#7848,.T.);
#11402=ORIENTED_EDGE('',*,*,#7864,.F.);
#11403=ORIENTED_EDGE('',*,*,#7846,.F.);
#11404=ORIENTED_EDGE('',*,*,#7865,.T.);
#11405=ORIENTED_EDGE('',*,*,#7866,.T.);
#11406=ORIENTED_EDGE('',*,*,#7865,.F.);
#11407=ORIENTED_EDGE('',*,*,#7866,.F.);
#11408=ORIENTED_EDGE('',*,*,#7859,.T.);
#11409=ORIENTED_EDGE('',*,*,#7863,.T.);
#11410=ORIENTED_EDGE('',*,*,#7862,.F.);
#11411=ORIENTED_EDGE('',*,*,#7867,.T.);
#11412=ORIENTED_EDGE('',*,*,#7867,.F.);
#11413=ORIENTED_EDGE('',*,*,#7868,.T.);
#11414=ORIENTED_EDGE('',*,*,#7868,.F.);
#11415=ORIENTED_EDGE('',*,*,#7869,.T.);
#11416=ORIENTED_EDGE('',*,*,#7869,.F.);
#11417=ORIENTED_EDGE('',*,*,#7870,.T.);
#11418=ORIENTED_EDGE('',*,*,#7870,.F.);
#11419=ORIENTED_EDGE('',*,*,#7871,.T.);
#11420=ORIENTED_EDGE('',*,*,#7871,.F.);
#11421=ORIENTED_EDGE('',*,*,#7872,.T.);
#11422=ORIENTED_EDGE('',*,*,#7872,.F.);
#11423=ORIENTED_EDGE('',*,*,#7873,.T.);
#11424=ORIENTED_EDGE('',*,*,#7873,.F.);
#11425=ORIENTED_EDGE('',*,*,#7874,.T.);
#11426=ORIENTED_EDGE('',*,*,#7875,.T.);
#11427=ORIENTED_EDGE('',*,*,#7876,.T.);
#11428=ORIENTED_EDGE('',*,*,#7877,.T.);
#11429=ORIENTED_EDGE('',*,*,#7875,.F.);
#11430=ORIENTED_EDGE('',*,*,#7878,.T.);
#11431=ORIENTED_EDGE('',*,*,#7879,.T.);
#11432=ORIENTED_EDGE('',*,*,#7880,.T.);
#11433=ORIENTED_EDGE('',*,*,#7879,.F.);
#11434=ORIENTED_EDGE('',*,*,#7881,.T.);
#11435=ORIENTED_EDGE('',*,*,#7882,.T.);
#11436=ORIENTED_EDGE('',*,*,#7883,.T.);
#11437=ORIENTED_EDGE('',*,*,#7882,.F.);
#11438=ORIENTED_EDGE('',*,*,#7884,.T.);
#11439=ORIENTED_EDGE('',*,*,#7885,.T.);
#11440=ORIENTED_EDGE('',*,*,#7886,.T.);
#11441=ORIENTED_EDGE('',*,*,#7885,.F.);
#11442=ORIENTED_EDGE('',*,*,#7887,.T.);
#11443=ORIENTED_EDGE('',*,*,#7888,.F.);
#11444=ORIENTED_EDGE('',*,*,#7889,.T.);
#11445=ORIENTED_EDGE('',*,*,#7890,.T.);
#11446=ORIENTED_EDGE('',*,*,#7889,.F.);
#11447=ORIENTED_EDGE('',*,*,#7877,.F.);
#11448=ORIENTED_EDGE('',*,*,#7891,.T.);
#11449=ORIENTED_EDGE('',*,*,#7892,.T.);
#11450=ORIENTED_EDGE('',*,*,#7891,.F.);
#11451=ORIENTED_EDGE('',*,*,#7876,.F.);
#11452=ORIENTED_EDGE('',*,*,#7893,.F.);
#11453=ORIENTED_EDGE('',*,*,#7894,.T.);
#11454=ORIENTED_EDGE('',*,*,#7887,.F.);
#11455=ORIENTED_EDGE('',*,*,#7884,.F.);
#11456=ORIENTED_EDGE('',*,*,#7894,.F.);
#11457=ORIENTED_EDGE('',*,*,#7893,.T.);
#11458=ORIENTED_EDGE('',*,*,#7895,.T.);
#11459=ORIENTED_EDGE('',*,*,#7896,.F.);
#11460=ORIENTED_EDGE('',*,*,#7895,.F.);
#11461=ORIENTED_EDGE('',*,*,#7878,.F.);
#11462=ORIENTED_EDGE('',*,*,#7897,.T.);
#11463=ORIENTED_EDGE('',*,*,#7896,.T.);
#11464=ORIENTED_EDGE('',*,*,#7897,.F.);
#11465=ORIENTED_EDGE('',*,*,#7898,.F.);
#11466=ORIENTED_EDGE('',*,*,#7899,.T.);
#11467=ORIENTED_EDGE('',*,*,#7883,.F.);
#11468=ORIENTED_EDGE('',*,*,#7899,.F.);
#11469=ORIENTED_EDGE('',*,*,#7900,.F.);
#11470=ORIENTED_EDGE('',*,*,#7901,.T.);
#11471=ORIENTED_EDGE('',*,*,#7902,.T.);
#11472=ORIENTED_EDGE('',*,*,#7901,.F.);
#11473=ORIENTED_EDGE('',*,*,#7903,.T.);
#11474=ORIENTED_EDGE('',*,*,#7904,.T.);
#11475=ORIENTED_EDGE('',*,*,#7905,.F.);
#11476=ORIENTED_EDGE('',*,*,#7904,.F.);
#11477=ORIENTED_EDGE('',*,*,#7906,.F.);
#11478=ORIENTED_EDGE('',*,*,#7907,.F.);
#11479=ORIENTED_EDGE('',*,*,#7908,.T.);
#11480=ORIENTED_EDGE('',*,*,#7909,.T.);
#11481=ORIENTED_EDGE('',*,*,#7908,.F.);
#11482=ORIENTED_EDGE('',*,*,#7903,.F.);
#11483=ORIENTED_EDGE('',*,*,#7910,.T.);
#11484=ORIENTED_EDGE('',*,*,#7906,.T.);
#11485=ORIENTED_EDGE('',*,*,#7907,.T.);
#11486=ORIENTED_EDGE('',*,*,#7910,.F.);
#11487=ORIENTED_EDGE('',*,*,#7909,.F.);
#11488=ORIENTED_EDGE('',*,*,#7874,.F.);
#11489=ORIENTED_EDGE('',*,*,#7905,.T.);
#11490=ORIENTED_EDGE('',*,*,#7881,.F.);
#11491=ORIENTED_EDGE('',*,*,#7900,.T.);
#11492=ORIENTED_EDGE('',*,*,#7886,.F.);
#11493=ORIENTED_EDGE('',*,*,#7902,.F.);
#11494=ORIENTED_EDGE('',*,*,#7898,.T.);
#11495=ORIENTED_EDGE('',*,*,#7888,.T.);
#11496=ORIENTED_EDGE('',*,*,#7892,.F.);
#11497=ORIENTED_EDGE('',*,*,#7890,.F.);
#11498=ORIENTED_EDGE('',*,*,#7880,.F.);
#11499=ORIENTED_EDGE('',*,*,#7911,.T.);
#11500=ORIENTED_EDGE('',*,*,#7912,.T.);
#11501=ORIENTED_EDGE('',*,*,#7913,.F.);
#11502=ORIENTED_EDGE('',*,*,#7912,.F.);
#11503=ORIENTED_EDGE('',*,*,#7914,.T.);
#11504=ORIENTED_EDGE('',*,*,#7915,.F.);
#11505=ORIENTED_EDGE('',*,*,#7916,.F.);
#11506=ORIENTED_EDGE('',*,*,#7917,.F.);
#11507=ORIENTED_EDGE('',*,*,#7918,.T.);
#11508=ORIENTED_EDGE('',*,*,#7919,.F.);
#11509=ORIENTED_EDGE('',*,*,#7920,.F.);
#11510=ORIENTED_EDGE('',*,*,#7921,.F.);
#11511=ORIENTED_EDGE('',*,*,#7922,.F.);
#11512=ORIENTED_EDGE('',*,*,#7923,.F.);
#11513=ORIENTED_EDGE('',*,*,#7924,.T.);
#11514=ORIENTED_EDGE('',*,*,#7925,.F.);
#11515=ORIENTED_EDGE('',*,*,#7926,.F.);
#11516=ORIENTED_EDGE('',*,*,#7927,.T.);
#11517=ORIENTED_EDGE('',*,*,#7928,.F.);
#11518=ORIENTED_EDGE('',*,*,#7929,.F.);
#11519=ORIENTED_EDGE('',*,*,#7930,.T.);
#11520=ORIENTED_EDGE('',*,*,#7931,.F.);
#11521=ORIENTED_EDGE('',*,*,#7932,.F.);
#11522=ORIENTED_EDGE('',*,*,#7927,.F.);
#11523=ORIENTED_EDGE('',*,*,#7933,.T.);
#11524=ORIENTED_EDGE('',*,*,#7934,.F.);
#11525=ORIENTED_EDGE('',*,*,#7935,.T.);
#11526=ORIENTED_EDGE('',*,*,#7936,.T.);
#11527=ORIENTED_EDGE('',*,*,#7937,.F.);
#11528=ORIENTED_EDGE('',*,*,#7936,.F.);
#11529=ORIENTED_EDGE('',*,*,#7938,.T.);
#11530=ORIENTED_EDGE('',*,*,#7939,.F.);
#11531=ORIENTED_EDGE('',*,*,#7940,.F.);
#11532=ORIENTED_EDGE('',*,*,#7941,.F.);
#11533=ORIENTED_EDGE('',*,*,#7942,.T.);
#11534=ORIENTED_EDGE('',*,*,#7943,.F.);
#11535=ORIENTED_EDGE('',*,*,#7944,.F.);
#11536=ORIENTED_EDGE('',*,*,#7945,.F.);
#11537=ORIENTED_EDGE('',*,*,#7946,.F.);
#11538=ORIENTED_EDGE('',*,*,#7947,.F.);
#11539=ORIENTED_EDGE('',*,*,#7948,.T.);
#11540=ORIENTED_EDGE('',*,*,#7949,.F.);
#11541=ORIENTED_EDGE('',*,*,#7950,.F.);
#11542=ORIENTED_EDGE('',*,*,#7951,.T.);
#11543=ORIENTED_EDGE('',*,*,#7952,.F.);
#11544=ORIENTED_EDGE('',*,*,#7953,.F.);
#11545=ORIENTED_EDGE('',*,*,#7954,.T.);
#11546=ORIENTED_EDGE('',*,*,#7955,.F.);
#11547=ORIENTED_EDGE('',*,*,#7956,.F.);
#11548=ORIENTED_EDGE('',*,*,#7951,.F.);
#11549=ORIENTED_EDGE('',*,*,#7957,.T.);
#11550=ORIENTED_EDGE('',*,*,#7958,.F.);
#11551=ORIENTED_EDGE('',*,*,#7959,.T.);
#11552=ORIENTED_EDGE('',*,*,#7960,.T.);
#11553=ORIENTED_EDGE('',*,*,#7961,.F.);
#11554=ORIENTED_EDGE('',*,*,#7960,.F.);
#11555=ORIENTED_EDGE('',*,*,#7962,.T.);
#11556=ORIENTED_EDGE('',*,*,#7963,.F.);
#11557=ORIENTED_EDGE('',*,*,#7964,.F.);
#11558=ORIENTED_EDGE('',*,*,#7965,.F.);
#11559=ORIENTED_EDGE('',*,*,#7966,.T.);
#11560=ORIENTED_EDGE('',*,*,#7967,.F.);
#11561=ORIENTED_EDGE('',*,*,#7968,.F.);
#11562=ORIENTED_EDGE('',*,*,#7969,.F.);
#11563=ORIENTED_EDGE('',*,*,#7970,.F.);
#11564=ORIENTED_EDGE('',*,*,#7971,.F.);
#11565=ORIENTED_EDGE('',*,*,#7972,.T.);
#11566=ORIENTED_EDGE('',*,*,#7973,.F.);
#11567=ORIENTED_EDGE('',*,*,#7974,.F.);
#11568=ORIENTED_EDGE('',*,*,#7975,.T.);
#11569=ORIENTED_EDGE('',*,*,#7976,.F.);
#11570=ORIENTED_EDGE('',*,*,#7977,.F.);
#11571=ORIENTED_EDGE('',*,*,#7978,.T.);
#11572=ORIENTED_EDGE('',*,*,#7979,.F.);
#11573=ORIENTED_EDGE('',*,*,#7980,.F.);
#11574=ORIENTED_EDGE('',*,*,#7975,.F.);
#11575=ORIENTED_EDGE('',*,*,#7981,.T.);
#11576=ORIENTED_EDGE('',*,*,#7982,.F.);
#11577=ORIENTED_EDGE('',*,*,#7983,.T.);
#11578=ORIENTED_EDGE('',*,*,#7984,.T.);
#11579=ORIENTED_EDGE('',*,*,#7985,.F.);
#11580=ORIENTED_EDGE('',*,*,#7984,.F.);
#11581=ORIENTED_EDGE('',*,*,#7986,.T.);
#11582=ORIENTED_EDGE('',*,*,#7987,.F.);
#11583=ORIENTED_EDGE('',*,*,#7988,.F.);
#11584=ORIENTED_EDGE('',*,*,#7989,.F.);
#11585=ORIENTED_EDGE('',*,*,#7990,.T.);
#11586=ORIENTED_EDGE('',*,*,#7991,.F.);
#11587=ORIENTED_EDGE('',*,*,#7992,.F.);
#11588=ORIENTED_EDGE('',*,*,#7993,.F.);
#11589=ORIENTED_EDGE('',*,*,#7994,.F.);
#11590=ORIENTED_EDGE('',*,*,#7995,.F.);
#11591=ORIENTED_EDGE('',*,*,#7996,.T.);
#11592=ORIENTED_EDGE('',*,*,#7997,.F.);
#11593=ORIENTED_EDGE('',*,*,#7998,.F.);
#11594=ORIENTED_EDGE('',*,*,#7999,.T.);
#11595=ORIENTED_EDGE('',*,*,#8000,.F.);
#11596=ORIENTED_EDGE('',*,*,#8001,.F.);
#11597=ORIENTED_EDGE('',*,*,#8002,.T.);
#11598=ORIENTED_EDGE('',*,*,#8003,.F.);
#11599=ORIENTED_EDGE('',*,*,#8004,.F.);
#11600=ORIENTED_EDGE('',*,*,#7999,.F.);
#11601=ORIENTED_EDGE('',*,*,#8005,.T.);
#11602=ORIENTED_EDGE('',*,*,#8006,.F.);
#11603=ORIENTED_EDGE('',*,*,#8007,.T.);
#11604=ORIENTED_EDGE('',*,*,#8008,.T.);
#11605=ORIENTED_EDGE('',*,*,#8009,.F.);
#11606=ORIENTED_EDGE('',*,*,#8008,.F.);
#11607=ORIENTED_EDGE('',*,*,#8010,.T.);
#11608=ORIENTED_EDGE('',*,*,#8011,.F.);
#11609=ORIENTED_EDGE('',*,*,#8012,.F.);
#11610=ORIENTED_EDGE('',*,*,#8013,.F.);
#11611=ORIENTED_EDGE('',*,*,#8014,.T.);
#11612=ORIENTED_EDGE('',*,*,#8015,.F.);
#11613=ORIENTED_EDGE('',*,*,#8016,.F.);
#11614=ORIENTED_EDGE('',*,*,#8017,.F.);
#11615=ORIENTED_EDGE('',*,*,#8018,.F.);
#11616=ORIENTED_EDGE('',*,*,#8019,.F.);
#11617=ORIENTED_EDGE('',*,*,#8020,.T.);
#11618=ORIENTED_EDGE('',*,*,#8021,.F.);
#11619=ORIENTED_EDGE('',*,*,#8022,.F.);
#11620=ORIENTED_EDGE('',*,*,#8023,.T.);
#11621=ORIENTED_EDGE('',*,*,#8024,.F.);
#11622=ORIENTED_EDGE('',*,*,#8025,.F.);
#11623=ORIENTED_EDGE('',*,*,#8026,.T.);
#11624=ORIENTED_EDGE('',*,*,#8027,.F.);
#11625=ORIENTED_EDGE('',*,*,#8028,.F.);
#11626=ORIENTED_EDGE('',*,*,#8023,.F.);
#11627=ORIENTED_EDGE('',*,*,#8029,.T.);
#11628=ORIENTED_EDGE('',*,*,#8030,.F.);
#11629=ORIENTED_EDGE('',*,*,#8031,.T.);
#11630=ORIENTED_EDGE('',*,*,#8032,.T.);
#11631=ORIENTED_EDGE('',*,*,#8033,.F.);
#11632=ORIENTED_EDGE('',*,*,#8032,.F.);
#11633=ORIENTED_EDGE('',*,*,#8034,.T.);
#11634=ORIENTED_EDGE('',*,*,#8035,.T.);
#11635=ORIENTED_EDGE('',*,*,#8036,.T.);
#11636=ORIENTED_EDGE('',*,*,#8037,.F.);
#11637=ORIENTED_EDGE('',*,*,#8038,.T.);
#11638=ORIENTED_EDGE('',*,*,#8039,.F.);
#11639=ORIENTED_EDGE('',*,*,#8040,.F.);
#11640=ORIENTED_EDGE('',*,*,#8041,.F.);
#11641=ORIENTED_EDGE('',*,*,#8042,.T.);
#11642=ORIENTED_EDGE('',*,*,#8043,.T.);
#11643=ORIENTED_EDGE('',*,*,#8044,.F.);
#11644=ORIENTED_EDGE('',*,*,#8045,.F.);
#11645=ORIENTED_EDGE('',*,*,#8046,.T.);
#11646=ORIENTED_EDGE('',*,*,#8047,.F.);
#11647=ORIENTED_EDGE('',*,*,#8048,.F.);
#11648=ORIENTED_EDGE('',*,*,#8043,.F.);
#11649=ORIENTED_EDGE('',*,*,#8049,.T.);
#11650=ORIENTED_EDGE('',*,*,#8050,.T.);
#11651=ORIENTED_EDGE('',*,*,#8051,.F.);
#11652=ORIENTED_EDGE('',*,*,#8052,.T.);
#11653=ORIENTED_EDGE('',*,*,#8053,.T.);
#11654=ORIENTED_EDGE('',*,*,#8054,.F.);
#11655=ORIENTED_EDGE('',*,*,#8055,.F.);
#11656=ORIENTED_EDGE('',*,*,#8056,.F.);
#11657=ORIENTED_EDGE('',*,*,#8057,.T.);
#11658=ORIENTED_EDGE('',*,*,#8058,.F.);
#11659=ORIENTED_EDGE('',*,*,#8059,.F.);
#11660=ORIENTED_EDGE('',*,*,#8060,.T.);
#11661=ORIENTED_EDGE('',*,*,#8061,.F.);
#11662=ORIENTED_EDGE('',*,*,#8062,.F.);
#11663=ORIENTED_EDGE('',*,*,#8063,.T.);
#11664=ORIENTED_EDGE('',*,*,#8064,.F.);
#11665=ORIENTED_EDGE('',*,*,#8065,.F.);
#11666=ORIENTED_EDGE('',*,*,#8060,.F.);
#11667=ORIENTED_EDGE('',*,*,#8066,.T.);
#11668=ORIENTED_EDGE('',*,*,#8067,.F.);
#11669=ORIENTED_EDGE('',*,*,#8068,.T.);
#11670=ORIENTED_EDGE('',*,*,#8069,.T.);
#11671=ORIENTED_EDGE('',*,*,#8070,.F.);
#11672=ORIENTED_EDGE('',*,*,#8069,.F.);
#11673=ORIENTED_EDGE('',*,*,#8071,.T.);
#11674=ORIENTED_EDGE('',*,*,#8072,.F.);
#11675=ORIENTED_EDGE('',*,*,#8073,.F.);
#11676=ORIENTED_EDGE('',*,*,#8074,.F.);
#11677=ORIENTED_EDGE('',*,*,#8075,.T.);
#11678=ORIENTED_EDGE('',*,*,#8076,.F.);
#11679=ORIENTED_EDGE('',*,*,#8077,.F.);
#11680=ORIENTED_EDGE('',*,*,#8078,.F.);
#11681=ORIENTED_EDGE('',*,*,#8079,.F.);
#11682=ORIENTED_EDGE('',*,*,#8076,.T.);
#11683=ORIENTED_EDGE('',*,*,#8080,.T.);
#11684=ORIENTED_EDGE('',*,*,#8036,.F.);
#11685=ORIENTED_EDGE('',*,*,#8081,.T.);
#11686=ORIENTED_EDGE('',*,*,#8078,.T.);
#11687=ORIENTED_EDGE('',*,*,#8082,.F.);
#11688=ORIENTED_EDGE('',*,*,#8034,.F.);
#11689=ORIENTED_EDGE('',*,*,#8037,.T.);
#11690=ORIENTED_EDGE('',*,*,#8080,.F.);
#11691=ORIENTED_EDGE('',*,*,#8075,.F.);
#11692=ORIENTED_EDGE('',*,*,#8081,.F.);
#11693=ORIENTED_EDGE('',*,*,#8082,.T.);
#11694=ORIENTED_EDGE('',*,*,#8077,.T.);
#11695=ORIENTED_EDGE('',*,*,#8079,.T.);
#11696=ORIENTED_EDGE('',*,*,#8035,.F.);
#11697=ORIENTED_EDGE('',*,*,#8068,.F.);
#11698=ORIENTED_EDGE('',*,*,#8067,.T.);
#11699=ORIENTED_EDGE('',*,*,#8070,.T.);
#11700=ORIENTED_EDGE('',*,*,#8066,.F.);
#11701=ORIENTED_EDGE('',*,*,#8083,.F.);
#11702=ORIENTED_EDGE('',*,*,#8057,.F.);
#11703=ORIENTED_EDGE('',*,*,#8084,.F.);
#11704=ORIENTED_EDGE('',*,*,#8063,.F.);
#11705=ORIENTED_EDGE('',*,*,#8061,.T.);
#11706=ORIENTED_EDGE('',*,*,#8065,.T.);
#11707=ORIENTED_EDGE('',*,*,#8085,.T.);
#11708=ORIENTED_EDGE('',*,*,#8055,.T.);
#11709=ORIENTED_EDGE('',*,*,#8059,.T.);
#11710=ORIENTED_EDGE('',*,*,#8086,.T.);
#11711=ORIENTED_EDGE('',*,*,#8064,.T.);
#11712=ORIENTED_EDGE('',*,*,#8084,.T.);
#11713=ORIENTED_EDGE('',*,*,#8056,.T.);
#11714=ORIENTED_EDGE('',*,*,#8085,.F.);
#11715=ORIENTED_EDGE('',*,*,#8062,.T.);
#11716=ORIENTED_EDGE('',*,*,#8086,.F.);
#11717=ORIENTED_EDGE('',*,*,#8058,.T.);
#11718=ORIENTED_EDGE('',*,*,#8083,.T.);
#11719=ORIENTED_EDGE('',*,*,#8033,.T.);
#11720=ORIENTED_EDGE('',*,*,#8053,.F.);
#11721=ORIENTED_EDGE('',*,*,#8031,.F.);
#11722=ORIENTED_EDGE('',*,*,#8054,.T.);
#11723=ORIENTED_EDGE('',*,*,#8012,.T.);
#11724=ORIENTED_EDGE('',*,*,#8087,.T.);
#11725=ORIENTED_EDGE('',*,*,#8040,.T.);
#11726=ORIENTED_EDGE('',*,*,#8088,.T.);
#11727=ORIENTED_EDGE('',*,*,#8089,.F.);
#11728=ORIENTED_EDGE('',*,*,#8038,.F.);
#11729=ORIENTED_EDGE('',*,*,#8090,.F.);
#11730=ORIENTED_EDGE('',*,*,#8010,.F.);
#11731=ORIENTED_EDGE('',*,*,#8011,.T.);
#11732=ORIENTED_EDGE('',*,*,#8090,.T.);
#11733=ORIENTED_EDGE('',*,*,#8041,.T.);
#11734=ORIENTED_EDGE('',*,*,#8087,.F.);
#11735=ORIENTED_EDGE('',*,*,#8013,.T.);
#11736=ORIENTED_EDGE('',*,*,#8088,.F.);
#11737=ORIENTED_EDGE('',*,*,#8039,.T.);
#11738=ORIENTED_EDGE('',*,*,#8089,.T.);
#11739=ORIENTED_EDGE('',*,*,#8025,.T.);
#11740=ORIENTED_EDGE('',*,*,#8091,.F.);
#11741=ORIENTED_EDGE('',*,*,#8021,.T.);
#11742=ORIENTED_EDGE('',*,*,#8092,.T.);
#11743=ORIENTED_EDGE('',*,*,#8027,.T.);
#11744=ORIENTED_EDGE('',*,*,#8093,.T.);
#11745=ORIENTED_EDGE('',*,*,#8019,.T.);
#11746=ORIENTED_EDGE('',*,*,#8094,.F.);
#11747=ORIENTED_EDGE('',*,*,#8024,.T.);
#11748=ORIENTED_EDGE('',*,*,#8028,.T.);
#11749=ORIENTED_EDGE('',*,*,#8094,.T.);
#11750=ORIENTED_EDGE('',*,*,#8018,.T.);
#11751=ORIENTED_EDGE('',*,*,#8022,.T.);
#11752=ORIENTED_EDGE('',*,*,#8091,.T.);
#11753=ORIENTED_EDGE('',*,*,#8092,.F.);
#11754=ORIENTED_EDGE('',*,*,#8020,.F.);
#11755=ORIENTED_EDGE('',*,*,#8093,.F.);
#11756=ORIENTED_EDGE('',*,*,#8026,.F.);
#11757=ORIENTED_EDGE('',*,*,#8009,.T.);
#11758=ORIENTED_EDGE('',*,*,#8029,.F.);
#11759=ORIENTED_EDGE('',*,*,#8007,.F.);
#11760=ORIENTED_EDGE('',*,*,#8030,.T.);
#11761=ORIENTED_EDGE('',*,*,#7988,.T.);
#11762=ORIENTED_EDGE('',*,*,#8095,.T.);
#11763=ORIENTED_EDGE('',*,*,#8016,.T.);
#11764=ORIENTED_EDGE('',*,*,#8096,.T.);
#11765=ORIENTED_EDGE('',*,*,#8097,.F.);
#11766=ORIENTED_EDGE('',*,*,#8014,.F.);
#11767=ORIENTED_EDGE('',*,*,#8098,.F.);
#11768=ORIENTED_EDGE('',*,*,#7986,.F.);
#11769=ORIENTED_EDGE('',*,*,#7987,.T.);
#11770=ORIENTED_EDGE('',*,*,#8098,.T.);
#11771=ORIENTED_EDGE('',*,*,#8017,.T.);
#11772=ORIENTED_EDGE('',*,*,#8095,.F.);
#11773=ORIENTED_EDGE('',*,*,#7989,.T.);
#11774=ORIENTED_EDGE('',*,*,#8096,.F.);
#11775=ORIENTED_EDGE('',*,*,#8015,.T.);
#11776=ORIENTED_EDGE('',*,*,#8097,.T.);
#11777=ORIENTED_EDGE('',*,*,#8001,.T.);
#11778=ORIENTED_EDGE('',*,*,#8099,.F.);
#11779=ORIENTED_EDGE('',*,*,#7997,.T.);
#11780=ORIENTED_EDGE('',*,*,#8100,.T.);
#11781=ORIENTED_EDGE('',*,*,#8003,.T.);
#11782=ORIENTED_EDGE('',*,*,#8101,.T.);
#11783=ORIENTED_EDGE('',*,*,#7995,.T.);
#11784=ORIENTED_EDGE('',*,*,#8102,.F.);
#11785=ORIENTED_EDGE('',*,*,#8000,.T.);
#11786=ORIENTED_EDGE('',*,*,#8004,.T.);
#11787=ORIENTED_EDGE('',*,*,#8102,.T.);
#11788=ORIENTED_EDGE('',*,*,#7994,.T.);
#11789=ORIENTED_EDGE('',*,*,#7998,.T.);
#11790=ORIENTED_EDGE('',*,*,#8099,.T.);
#11791=ORIENTED_EDGE('',*,*,#8100,.F.);
#11792=ORIENTED_EDGE('',*,*,#7996,.F.);
#11793=ORIENTED_EDGE('',*,*,#8101,.F.);
#11794=ORIENTED_EDGE('',*,*,#8002,.F.);
#11795=ORIENTED_EDGE('',*,*,#7985,.T.);
#11796=ORIENTED_EDGE('',*,*,#8005,.F.);
#11797=ORIENTED_EDGE('',*,*,#7983,.F.);
#11798=ORIENTED_EDGE('',*,*,#8006,.T.);
#11799=ORIENTED_EDGE('',*,*,#7964,.T.);
#11800=ORIENTED_EDGE('',*,*,#8103,.T.);
#11801=ORIENTED_EDGE('',*,*,#7992,.T.);
#11802=ORIENTED_EDGE('',*,*,#8104,.T.);
#11803=ORIENTED_EDGE('',*,*,#8105,.F.);
#11804=ORIENTED_EDGE('',*,*,#7990,.F.);
#11805=ORIENTED_EDGE('',*,*,#8106,.F.);
#11806=ORIENTED_EDGE('',*,*,#7962,.F.);
#11807=ORIENTED_EDGE('',*,*,#7963,.T.);
#11808=ORIENTED_EDGE('',*,*,#8106,.T.);
#11809=ORIENTED_EDGE('',*,*,#7993,.T.);
#11810=ORIENTED_EDGE('',*,*,#8103,.F.);
#11811=ORIENTED_EDGE('',*,*,#7965,.T.);
#11812=ORIENTED_EDGE('',*,*,#8104,.F.);
#11813=ORIENTED_EDGE('',*,*,#7991,.T.);
#11814=ORIENTED_EDGE('',*,*,#8105,.T.);
#11815=ORIENTED_EDGE('',*,*,#7977,.T.);
#11816=ORIENTED_EDGE('',*,*,#8107,.F.);
#11817=ORIENTED_EDGE('',*,*,#7973,.T.);
#11818=ORIENTED_EDGE('',*,*,#8108,.T.);
#11819=ORIENTED_EDGE('',*,*,#7979,.T.);
#11820=ORIENTED_EDGE('',*,*,#8109,.T.);
#11821=ORIENTED_EDGE('',*,*,#7971,.T.);
#11822=ORIENTED_EDGE('',*,*,#8110,.F.);
#11823=ORIENTED_EDGE('',*,*,#7976,.T.);
#11824=ORIENTED_EDGE('',*,*,#7980,.T.);
#11825=ORIENTED_EDGE('',*,*,#8110,.T.);
#11826=ORIENTED_EDGE('',*,*,#7970,.T.);
#11827=ORIENTED_EDGE('',*,*,#7974,.T.);
#11828=ORIENTED_EDGE('',*,*,#8107,.T.);
#11829=ORIENTED_EDGE('',*,*,#8108,.F.);
#11830=ORIENTED_EDGE('',*,*,#7972,.F.);
#11831=ORIENTED_EDGE('',*,*,#8109,.F.);
#11832=ORIENTED_EDGE('',*,*,#7978,.F.);
#11833=ORIENTED_EDGE('',*,*,#7961,.T.);
#11834=ORIENTED_EDGE('',*,*,#7981,.F.);
#11835=ORIENTED_EDGE('',*,*,#7959,.F.);
#11836=ORIENTED_EDGE('',*,*,#7982,.T.);
#11837=ORIENTED_EDGE('',*,*,#7940,.T.);
#11838=ORIENTED_EDGE('',*,*,#8111,.T.);
#11839=ORIENTED_EDGE('',*,*,#7968,.T.);
#11840=ORIENTED_EDGE('',*,*,#8112,.T.);
#11841=ORIENTED_EDGE('',*,*,#8113,.F.);
#11842=ORIENTED_EDGE('',*,*,#7966,.F.);
#11843=ORIENTED_EDGE('',*,*,#8114,.F.);
#11844=ORIENTED_EDGE('',*,*,#7938,.F.);
#11845=ORIENTED_EDGE('',*,*,#7939,.T.);
#11846=ORIENTED_EDGE('',*,*,#8114,.T.);
#11847=ORIENTED_EDGE('',*,*,#7969,.T.);
#11848=ORIENTED_EDGE('',*,*,#8111,.F.);
#11849=ORIENTED_EDGE('',*,*,#7941,.T.);
#11850=ORIENTED_EDGE('',*,*,#8112,.F.);
#11851=ORIENTED_EDGE('',*,*,#7967,.T.);
#11852=ORIENTED_EDGE('',*,*,#8113,.T.);
#11853=ORIENTED_EDGE('',*,*,#7953,.T.);
#11854=ORIENTED_EDGE('',*,*,#8115,.F.);
#11855=ORIENTED_EDGE('',*,*,#7949,.T.);
#11856=ORIENTED_EDGE('',*,*,#8116,.T.);
#11857=ORIENTED_EDGE('',*,*,#7955,.T.);
#11858=ORIENTED_EDGE('',*,*,#8117,.T.);
#11859=ORIENTED_EDGE('',*,*,#7947,.T.);
#11860=ORIENTED_EDGE('',*,*,#8118,.F.);
#11861=ORIENTED_EDGE('',*,*,#7952,.T.);
#11862=ORIENTED_EDGE('',*,*,#7956,.T.);
#11863=ORIENTED_EDGE('',*,*,#8118,.T.);
#11864=ORIENTED_EDGE('',*,*,#7946,.T.);
#11865=ORIENTED_EDGE('',*,*,#7950,.T.);
#11866=ORIENTED_EDGE('',*,*,#8115,.T.);
#11867=ORIENTED_EDGE('',*,*,#8116,.F.);
#11868=ORIENTED_EDGE('',*,*,#7948,.F.);
#11869=ORIENTED_EDGE('',*,*,#8117,.F.);
#11870=ORIENTED_EDGE('',*,*,#7954,.F.);
#11871=ORIENTED_EDGE('',*,*,#7937,.T.);
#11872=ORIENTED_EDGE('',*,*,#7957,.F.);
#11873=ORIENTED_EDGE('',*,*,#7935,.F.);
#11874=ORIENTED_EDGE('',*,*,#7958,.T.);
#11875=ORIENTED_EDGE('',*,*,#7916,.T.);
#11876=ORIENTED_EDGE('',*,*,#8119,.T.);
#11877=ORIENTED_EDGE('',*,*,#7944,.T.);
#11878=ORIENTED_EDGE('',*,*,#8120,.T.);
#11879=ORIENTED_EDGE('',*,*,#8121,.F.);
#11880=ORIENTED_EDGE('',*,*,#7942,.F.);
#11881=ORIENTED_EDGE('',*,*,#8122,.F.);
#11882=ORIENTED_EDGE('',*,*,#7914,.F.);
#11883=ORIENTED_EDGE('',*,*,#7915,.T.);
#11884=ORIENTED_EDGE('',*,*,#8122,.T.);
#11885=ORIENTED_EDGE('',*,*,#7945,.T.);
#11886=ORIENTED_EDGE('',*,*,#8119,.F.);
#11887=ORIENTED_EDGE('',*,*,#7917,.T.);
#11888=ORIENTED_EDGE('',*,*,#8120,.F.);
#11889=ORIENTED_EDGE('',*,*,#7943,.T.);
#11890=ORIENTED_EDGE('',*,*,#8121,.T.);
#11891=ORIENTED_EDGE('',*,*,#7929,.T.);
#11892=ORIENTED_EDGE('',*,*,#8123,.F.);
#11893=ORIENTED_EDGE('',*,*,#7925,.T.);
#11894=ORIENTED_EDGE('',*,*,#8124,.T.);
#11895=ORIENTED_EDGE('',*,*,#7931,.T.);
#11896=ORIENTED_EDGE('',*,*,#8125,.T.);
#11897=ORIENTED_EDGE('',*,*,#7923,.T.);
#11898=ORIENTED_EDGE('',*,*,#8126,.F.);
#11899=ORIENTED_EDGE('',*,*,#7928,.T.);
#11900=ORIENTED_EDGE('',*,*,#7932,.T.);
#11901=ORIENTED_EDGE('',*,*,#8126,.T.);
#11902=ORIENTED_EDGE('',*,*,#7922,.T.);
#11903=ORIENTED_EDGE('',*,*,#7926,.T.);
#11904=ORIENTED_EDGE('',*,*,#8123,.T.);
#11905=ORIENTED_EDGE('',*,*,#8124,.F.);
#11906=ORIENTED_EDGE('',*,*,#7924,.F.);
#11907=ORIENTED_EDGE('',*,*,#8125,.F.);
#11908=ORIENTED_EDGE('',*,*,#7930,.F.);
#11909=ORIENTED_EDGE('',*,*,#7913,.T.);
#11910=ORIENTED_EDGE('',*,*,#7933,.F.);
#11911=ORIENTED_EDGE('',*,*,#7911,.F.);
#11912=ORIENTED_EDGE('',*,*,#7934,.T.);
#11913=ORIENTED_EDGE('',*,*,#8073,.T.);
#11914=ORIENTED_EDGE('',*,*,#8127,.T.);
#11915=ORIENTED_EDGE('',*,*,#7920,.T.);
#11916=ORIENTED_EDGE('',*,*,#8128,.T.);
#11917=ORIENTED_EDGE('',*,*,#8129,.F.);
#11918=ORIENTED_EDGE('',*,*,#7918,.F.);
#11919=ORIENTED_EDGE('',*,*,#8130,.F.);
#11920=ORIENTED_EDGE('',*,*,#8071,.F.);
#11921=ORIENTED_EDGE('',*,*,#8072,.T.);
#11922=ORIENTED_EDGE('',*,*,#8130,.T.);
#11923=ORIENTED_EDGE('',*,*,#7921,.T.);
#11924=ORIENTED_EDGE('',*,*,#8127,.F.);
#11925=ORIENTED_EDGE('',*,*,#8074,.T.);
#11926=ORIENTED_EDGE('',*,*,#8128,.F.);
#11927=ORIENTED_EDGE('',*,*,#7919,.T.);
#11928=ORIENTED_EDGE('',*,*,#8129,.T.);
#11929=ORIENTED_EDGE('',*,*,#8051,.T.);
#11930=ORIENTED_EDGE('',*,*,#8131,.F.);
#11931=ORIENTED_EDGE('',*,*,#8046,.F.);
#11932=ORIENTED_EDGE('',*,*,#8132,.F.);
#11933=ORIENTED_EDGE('',*,*,#8133,.T.);
#11934=ORIENTED_EDGE('',*,*,#8044,.T.);
#11935=ORIENTED_EDGE('',*,*,#8048,.T.);
#11936=ORIENTED_EDGE('',*,*,#8134,.T.);
#11937=ORIENTED_EDGE('',*,*,#8049,.F.);
#11938=ORIENTED_EDGE('',*,*,#8042,.F.);
#11939=ORIENTED_EDGE('',*,*,#8134,.F.);
#11940=ORIENTED_EDGE('',*,*,#8047,.T.);
#11941=ORIENTED_EDGE('',*,*,#8131,.T.);
#11942=ORIENTED_EDGE('',*,*,#8050,.F.);
#11943=ORIENTED_EDGE('',*,*,#8132,.T.);
#11944=ORIENTED_EDGE('',*,*,#8045,.T.);
#11945=ORIENTED_EDGE('',*,*,#8133,.F.);
#11946=ORIENTED_EDGE('',*,*,#8052,.F.);
#12257=CYLINDRICAL_SURFACE('',#14584,7.5);
#12258=CYLINDRICAL_SURFACE('',#14587,12.4653846153846);
#12259=CYLINDRICAL_SURFACE('',#14589,12.4653846153846);
#12260=CYLINDRICAL_SURFACE('',#14625,17.6897435897436);
#12261=CYLINDRICAL_SURFACE('',#14628,16.2686153846154);
#12262=CYLINDRICAL_SURFACE('',#14630,16.0346153846154);
#12263=CYLINDRICAL_SURFACE('',#14635,16.0346153846154);
#12264=CYLINDRICAL_SURFACE('',#14636,16.2686153846154);
#12265=CYLINDRICAL_SURFACE('',#14638,17.6897435897436);
#12266=CYLINDRICAL_SURFACE('',#14648,21.);
#12267=CYLINDRICAL_SURFACE('',#14753,14.25);
#12268=CYLINDRICAL_SURFACE('',#14756,15.1423076923077);
#12269=CYLINDRICAL_SURFACE('',#14769,15.1423076923077);
#12270=CYLINDRICAL_SURFACE('',#14770,14.25);
#12271=CYLINDRICAL_SURFACE('',#14779,15.1423076923077);
#12272=CYLINDRICAL_SURFACE('',#14780,14.25);
#12273=CYLINDRICAL_SURFACE('',#14781,14.25);
#12274=CYLINDRICAL_SURFACE('',#14784,15.1423076923077);
#12275=CYLINDRICAL_SURFACE('',#14797,15.1423076923077);
#12276=CYLINDRICAL_SURFACE('',#14798,14.25);
#12277=CYLINDRICAL_SURFACE('',#14799,14.25);
#12278=CYLINDRICAL_SURFACE('',#14802,15.1423076923077);
#12279=CYLINDRICAL_SURFACE('',#14815,15.1423076923077);
#12280=CYLINDRICAL_SURFACE('',#14816,14.25);
#12281=CYLINDRICAL_SURFACE('',#14817,14.25);
#12282=CYLINDRICAL_SURFACE('',#14820,15.1423076923077);
#12283=CYLINDRICAL_SURFACE('',#14833,15.1423076923077);
#12284=CYLINDRICAL_SURFACE('',#14834,14.25);
#12285=CYLINDRICAL_SURFACE('',#14835,14.25);
#12286=CYLINDRICAL_SURFACE('',#14838,15.1423076923077);
#12287=CYLINDRICAL_SURFACE('',#14851,15.1423076923077);
#12288=CYLINDRICAL_SURFACE('',#14852,14.25);
#12289=CYLINDRICAL_SURFACE('',#14853,14.25);
#12290=CYLINDRICAL_SURFACE('',#14856,15.1423076923077);
#12291=CYLINDRICAL_SURFACE('',#14869,15.1423076923077);
#12292=CYLINDRICAL_SURFACE('',#14870,14.25);
#12293=CYLINDRICAL_SURFACE('',#14877,15.1423076923077);
#12294=CYLINDRICAL_SURFACE('',#14878,14.25);
#12914=ADVANCED_FACE('',(#1902),#160,.F.);
#12915=ADVANCED_FACE('',(#1903),#161,.T.);
#12916=ADVANCED_FACE('',(#1904),#162,.T.);
#12917=ADVANCED_FACE('',(#1905),#111,.F.);
#12918=ADVANCED_FACE('',(#1906),#12257,.F.);
#12919=ADVANCED_FACE('',(#1907),#112,.F.);
#12920=ADVANCED_FACE('',(#1908),#12258,.T.);
#12921=ADVANCED_FACE('',(#1909),#12259,.T.);
#12922=ADVANCED_FACE('',(#1910,#433),#1225,.T.);
#12923=ADVANCED_FACE('',(#1911,#434),#1226,.T.);
#12924=ADVANCED_FACE('',(#1912),#85,.T.);
#12925=ADVANCED_FACE('',(#1913),#86,.T.);
#12926=ADVANCED_FACE('',(#1914),#87,.T.);
#12927=ADVANCED_FACE('',(#1915),#88,.T.);
#12928=ADVANCED_FACE('',(#1916),#89,.T.);
#12929=ADVANCED_FACE('',(#1917),#90,.T.);
#12930=ADVANCED_FACE('',(#1918),#91,.T.);
#12931=ADVANCED_FACE('',(#1919),#163,.T.);
#12932=ADVANCED_FACE('',(#1920),#164,.T.);
#12933=ADVANCED_FACE('',(#1921),#165,.T.);
#12934=ADVANCED_FACE('',(#1922),#166,.T.);
#12935=ADVANCED_FACE('',(#1923),#12260,.F.);
#12936=ADVANCED_FACE('',(#1924),#12261,.F.);
#12937=ADVANCED_FACE('',(#1925),#12262,.F.);
#12938=ADVANCED_FACE('',(#1926),#167,.F.);
#12939=ADVANCED_FACE('',(#1927),#12263,.F.);
#12940=ADVANCED_FACE('',(#1928),#12264,.F.);
#12941=ADVANCED_FACE('',(#1929),#12265,.F.);
#12942=ADVANCED_FACE('',(#1930),#113,.T.);
#12943=ADVANCED_FACE('',(#1931),#114,.T.);
#12944=ADVANCED_FACE('',(#1932),#12266,.T.);
#12945=ADVANCED_FACE('',(#1933,#435),#1227,.T.);
#12946=ADVANCED_FACE('',(#1934,#436),#1228,.T.);
#12947=ADVANCED_FACE('',(#1935,#437),#1229,.F.);
#12948=ADVANCED_FACE('',(#1936,#438),#1230,.F.);
#12949=ADVANCED_FACE('',(#1937,#439),#1231,.F.);
#12950=ADVANCED_FACE('',(#1938,#440),#1232,.F.);
#12951=ADVANCED_FACE('',(#1939,#441,#442),#168,.T.);
#12952=ADVANCED_FACE('',(#1940,#443,#444),#92,.F.);
#12953=ADVANCED_FACE('',(#1941,#445,#446),#169,.T.);
#12954=ADVANCED_FACE('',(#1942,#447,#448),#93,.F.);
#12955=ADVANCED_FACE('',(#1943,#449,#450),#170,.T.);
#12956=ADVANCED_FACE('',(#1944,#451,#452),#94,.F.);
#12957=ADVANCED_FACE('',(#1945,#453,#454),#171,.T.);
#12958=ADVANCED_FACE('',(#1946,#455,#456),#95,.F.);
#12959=ADVANCED_FACE('',(#1947,#457,#458),#172,.T.);
#12960=ADVANCED_FACE('',(#1948,#459,#460),#96,.F.);
#12961=ADVANCED_FACE('',(#1949,#461,#462),#173,.T.);
#12962=ADVANCED_FACE('',(#1950,#463,#464),#97,.F.);
#12963=ADVANCED_FACE('',(#1951,#465,#466),#98,.F.);
#12964=ADVANCED_FACE('',(#1952,#467,#468),#174,.T.);
#12965=ADVANCED_FACE('',(#1953),#12267,.F.);
#12966=ADVANCED_FACE('',(#1954),#12268,.T.);
#12967=ADVANCED_FACE('',(#1955),#1233,.F.);
#12968=ADVANCED_FACE('',(#1956),#1234,.T.);
#12969=ADVANCED_FACE('',(#1957,#469),#1235,.F.);
#12970=ADVANCED_FACE('',(#1958,#470),#1236,.F.);
#12971=ADVANCED_FACE('',(#1959),#1237,.F.);
#12972=ADVANCED_FACE('',(#1960),#1238,.T.);
#12973=ADVANCED_FACE('',(#1961),#12269,.T.);
#12974=ADVANCED_FACE('',(#1962),#12270,.F.);
#12975=ADVANCED_FACE('',(#1963,#471),#1239,.F.);
#12976=ADVANCED_FACE('',(#1964,#472),#1240,.F.);
#12977=ADVANCED_FACE('',(#1965),#1241,.T.);
#12978=ADVANCED_FACE('',(#1966),#1242,.F.);
#12979=ADVANCED_FACE('',(#1967),#12271,.T.);
#12980=ADVANCED_FACE('',(#1968),#12272,.F.);
#12981=ADVANCED_FACE('',(#1969),#12273,.F.);
#12982=ADVANCED_FACE('',(#1970),#12274,.T.);
#12983=ADVANCED_FACE('',(#1971),#1243,.T.);
#12984=ADVANCED_FACE('',(#1972),#1244,.F.);
#12985=ADVANCED_FACE('',(#1973,#473),#1245,.F.);
#12986=ADVANCED_FACE('',(#1974,#474),#1246,.F.);
#12987=ADVANCED_FACE('',(#1975),#1247,.T.);
#12988=ADVANCED_FACE('',(#1976),#1248,.F.);
#12989=ADVANCED_FACE('',(#1977),#12275,.T.);
#12990=ADVANCED_FACE('',(#1978),#12276,.F.);
#12991=ADVANCED_FACE('',(#1979),#12277,.F.);
#12992=ADVANCED_FACE('',(#1980),#12278,.T.);
#12993=ADVANCED_FACE('',(#1981),#1249,.T.);
#12994=ADVANCED_FACE('',(#1982),#1250,.F.);
#12995=ADVANCED_FACE('',(#1983,#475),#1251,.F.);
#12996=ADVANCED_FACE('',(#1984,#476),#1252,.F.);
#12997=ADVANCED_FACE('',(#1985),#1253,.T.);
#12998=ADVANCED_FACE('',(#1986),#1254,.F.);
#12999=ADVANCED_FACE('',(#1987),#12279,.T.);
#13000=ADVANCED_FACE('',(#1988),#12280,.F.);
#13001=ADVANCED_FACE('',(#1989),#12281,.F.);
#13002=ADVANCED_FACE('',(#1990),#12282,.T.);
#13003=ADVANCED_FACE('',(#1991),#1255,.T.);
#13004=ADVANCED_FACE('',(#1992),#1256,.F.);
#13005=ADVANCED_FACE('',(#1993,#477),#1257,.F.);
#13006=ADVANCED_FACE('',(#1994,#478),#1258,.F.);
#13007=ADVANCED_FACE('',(#1995),#1259,.T.);
#13008=ADVANCED_FACE('',(#1996),#1260,.F.);
#13009=ADVANCED_FACE('',(#1997),#12283,.T.);
#13010=ADVANCED_FACE('',(#1998),#12284,.F.);
#13011=ADVANCED_FACE('',(#1999),#12285,.F.);
#13012=ADVANCED_FACE('',(#2000),#12286,.T.);
#13013=ADVANCED_FACE('',(#2001),#1261,.T.);
#13014=ADVANCED_FACE('',(#2002),#1262,.F.);
#13015=ADVANCED_FACE('',(#2003,#479),#1263,.F.);
#13016=ADVANCED_FACE('',(#2004,#480),#1264,.F.);
#13017=ADVANCED_FACE('',(#2005),#1265,.T.);
#13018=ADVANCED_FACE('',(#2006),#1266,.F.);
#13019=ADVANCED_FACE('',(#2007),#12287,.T.);
#13020=ADVANCED_FACE('',(#2008),#12288,.F.);
#13021=ADVANCED_FACE('',(#2009),#12289,.F.);
#13022=ADVANCED_FACE('',(#2010),#12290,.T.);
#13023=ADVANCED_FACE('',(#2011),#1267,.T.);
#13024=ADVANCED_FACE('',(#2012),#1268,.F.);
#13025=ADVANCED_FACE('',(#2013,#481),#1269,.F.);
#13026=ADVANCED_FACE('',(#2014,#482),#1270,.F.);
#13027=ADVANCED_FACE('',(#2015),#1271,.T.);
#13028=ADVANCED_FACE('',(#2016),#1272,.F.);
#13029=ADVANCED_FACE('',(#2017),#12291,.T.);
#13030=ADVANCED_FACE('',(#2018),#12292,.F.);
#13031=ADVANCED_FACE('',(#2019),#1273,.F.);
#13032=ADVANCED_FACE('',(#2020),#1274,.T.);
#13033=ADVANCED_FACE('',(#2021),#12293,.T.);
#13034=ADVANCED_FACE('',(#2022),#12294,.F.);
#13083=CLOSED_SHELL('',(#12914,#12915,#12916,#12917,#12918,#12919,#12920,
#12921,#12922,#12923));
#13084=CLOSED_SHELL('',(#12924));
#13085=CLOSED_SHELL('',(#12925));
#13086=CLOSED_SHELL('',(#12926));
#13087=CLOSED_SHELL('',(#12927));
#13088=CLOSED_SHELL('',(#12928));
#13089=CLOSED_SHELL('',(#12929));
#13090=CLOSED_SHELL('',(#12930));
#13091=CLOSED_SHELL('',(#12931,#12932,#12933,#12934,#12935,#12936,#12937,
#12938,#12939,#12940,#12941,#12942,#12943,#12944,#12945,#12946,#12947,#12948,
#12949,#12950));
#13092=CLOSED_SHELL('',(#12951,#12952,#12953,#12954,#12955,#12956,#12957,
#12958,#12959,#12960,#12961,#12962,#12963,#12964,#12965,#12966,#12967,#12968,
#12969,#12970,#12971,#12972,#12973,#12974,#12975,#12976,#12977,#12978,#12979,
#12980,#12981,#12982,#12983,#12984,#12985,#12986,#12987,#12988,#12989,#12990,
#12991,#12992,#12993,#12994,#12995,#12996,#12997,#12998,#12999,#13000,#13001,
#13002,#13003,#13004,#13005,#13006,#13007,#13008,#13009,#13010,#13011,#13012,
#13013,#13014,#13015,#13016,#13017,#13018,#13019,#13020,#13021,#13022,#13023,
#13024,#13025,#13026,#13027,#13028,#13029,#13030,#13031,#13032,#13033,#13034));
#14566=AXIS2_PLACEMENT_3D('',#42263,#18083,#18084);
#14567=AXIS2_PLACEMENT_3D('',#42264,#18085,#18086);
#14568=AXIS2_PLACEMENT_3D('',#42266,#18087,#18088);
#14569=AXIS2_PLACEMENT_3D('',#42268,#18089,#18090);
#14570=AXIS2_PLACEMENT_3D('',#42269,#18091,#18092);
#14571=AXIS2_PLACEMENT_3D('',#42270,#18093,#18094);
#14572=AXIS2_PLACEMENT_3D('',#42273,#18095,#18096);
#14573=AXIS2_PLACEMENT_3D('',#42275,#18097,#18098);
#14574=AXIS2_PLACEMENT_3D('',#42277,#18099,#18100);
#14575=AXIS2_PLACEMENT_3D('',#42278,#18101,#18102);
#14576=AXIS2_PLACEMENT_3D('',#42279,#18103,#18104);
#14577=AXIS2_PLACEMENT_3D('',#42280,#18105,#18106);
#14578=AXIS2_PLACEMENT_3D('',#42283,#18107,#18108);
#14579=AXIS2_PLACEMENT_3D('',#42285,#18109,#18110);
#14580=AXIS2_PLACEMENT_3D('',#42286,#18111,#18112);
#14581=AXIS2_PLACEMENT_3D('',#42287,#18113,#18114);
#14582=AXIS2_PLACEMENT_3D('',#42288,#18115,#18116);
#14583=AXIS2_PLACEMENT_3D('',#42291,#18118,#18119);
#14584=AXIS2_PLACEMENT_3D('',#42292,#18120,#18121);
#14585=AXIS2_PLACEMENT_3D('',#42294,#18123,#18124);
#14586=AXIS2_PLACEMENT_3D('',#42297,#18126,#18127);
#14587=AXIS2_PLACEMENT_3D('',#42298,#18128,#18129);
#14588=AXIS2_PLACEMENT_3D('',#42300,#18130,#18131);
#14589=AXIS2_PLACEMENT_3D('',#42302,#18133,#18134);
#14590=AXIS2_PLACEMENT_3D('',#42305,#18136,#18137);
#14591=AXIS2_PLACEMENT_3D('',#42306,#18138,#18139);
#14592=AXIS2_PLACEMENT_3D('',#42307,#18140,#18141);
#14593=AXIS2_PLACEMENT_3D('',#42308,#18142,#18143);
#14594=AXIS2_PLACEMENT_3D('',#42311,#18144,#18145);
#14595=AXIS2_PLACEMENT_3D('',#42312,#18146,#18147);
#14596=AXIS2_PLACEMENT_3D('',#42315,#18148,#18149);
#14597=AXIS2_PLACEMENT_3D('',#42316,#18150,#18151);
#14598=AXIS2_PLACEMENT_3D('',#42319,#18152,#18153);
#14599=AXIS2_PLACEMENT_3D('',#42320,#18154,#18155);
#14600=AXIS2_PLACEMENT_3D('',#42323,#18156,#18157);
#14601=AXIS2_PLACEMENT_3D('',#42324,#18158,#18159);
#14602=AXIS2_PLACEMENT_3D('',#42327,#18160,#18161);
#14603=AXIS2_PLACEMENT_3D('',#42328,#18162,#18163);
#14604=AXIS2_PLACEMENT_3D('',#42331,#18164,#18165);
#14605=AXIS2_PLACEMENT_3D('',#42332,#18166,#18167);
#14606=AXIS2_PLACEMENT_3D('',#42335,#18168,#18169);
#14607=AXIS2_PLACEMENT_3D('',#42336,#18170,#18171);
#14608=AXIS2_PLACEMENT_3D('',#42338,#18172,#18173);
#14609=AXIS2_PLACEMENT_3D('',#42340,#18174,#18175);
#14610=AXIS2_PLACEMENT_3D('',#42342,#18176,#18177);
#14611=AXIS2_PLACEMENT_3D('',#42343,#18178,#18179);
#14612=AXIS2_PLACEMENT_3D('',#42344,#18180,#18181);
#14613=AXIS2_PLACEMENT_3D('',#42346,#18182,#18183);
#14614=AXIS2_PLACEMENT_3D('',#42348,#18184,#18185);
#14615=AXIS2_PLACEMENT_3D('',#42349,#18186,#18187);
#14616=AXIS2_PLACEMENT_3D('',#42350,#18188,#18189);
#14617=AXIS2_PLACEMENT_3D('',#42352,#18190,#18191);
#14618=AXIS2_PLACEMENT_3D('',#42354,#18192,#18193);
#14619=AXIS2_PLACEMENT_3D('',#42355,#18194,#18195);
#14620=AXIS2_PLACEMENT_3D('',#42356,#18196,#18197);
#14621=AXIS2_PLACEMENT_3D('',#42359,#18198,#18199);
#14622=AXIS2_PLACEMENT_3D('',#42361,#18200,#18201);
#14623=AXIS2_PLACEMENT_3D('',#42362,#18202,#18203);
#14624=AXIS2_PLACEMENT_3D('',#42363,#18204,#18205);
#14625=AXIS2_PLACEMENT_3D('',#42364,#18206,#18207);
#14626=AXIS2_PLACEMENT_3D('',#42366,#18208,#18209);
#14627=AXIS2_PLACEMENT_3D('',#42369,#18211,#18212);
#14628=AXIS2_PLACEMENT_3D('',#42370,#18213,#18214);
#14629=AXIS2_PLACEMENT_3D('',#42373,#18216,#18217);
#14630=AXIS2_PLACEMENT_3D('',#42374,#18218,#18219);
#14631=AXIS2_PLACEMENT_3D('',#42376,#18220,#18221);
#14632=AXIS2_PLACEMENT_3D('',#42378,#18223,#18224);
#14633=AXIS2_PLACEMENT_3D('',#42380,#18225,#18226);
#14634=AXIS2_PLACEMENT_3D('',#42381,#18227,#18228);
#14635=AXIS2_PLACEMENT_3D('',#42382,#18229,#18230);
#14636=AXIS2_PLACEMENT_3D('',#42384,#18232,#18233);
#14637=AXIS2_PLACEMENT_3D('',#42386,#18234,#18235);
#14638=AXIS2_PLACEMENT_3D('',#42388,#18237,#18238);
#14639=AXIS2_PLACEMENT_3D('',#42390,#18239,#18240);
#14640=AXIS2_PLACEMENT_3D('',#42393,#18242,#18243);
#14641=AXIS2_PLACEMENT_3D('',#42394,#18244,#18245);
#14642=AXIS2_PLACEMENT_3D('',#42396,#18246,#18247);
#14643=AXIS2_PLACEMENT_3D('',#42399,#18249,#18250);
#14644=AXIS2_PLACEMENT_3D('',#42400,#18251,#18252);
#14645=AXIS2_PLACEMENT_3D('',#42403,#18253,#18254);
#14646=AXIS2_PLACEMENT_3D('',#42404,#18255,#18256);
#14647=AXIS2_PLACEMENT_3D('',#42407,#18258,#18259);
#14648=AXIS2_PLACEMENT_3D('',#42408,#18260,#18261);
#14649=AXIS2_PLACEMENT_3D('',#42410,#18263,#18264);
#14650=AXIS2_PLACEMENT_3D('',#42411,#18265,#18266);
#14651=AXIS2_PLACEMENT_3D('',#42412,#18267,#18268);
#14652=AXIS2_PLACEMENT_3D('',#42413,#18269,#18270);
#14653=AXIS2_PLACEMENT_3D('',#42414,#18271,#18272);
#14654=AXIS2_PLACEMENT_3D('',#42415,#18273,#18274);
#14655=AXIS2_PLACEMENT_3D('',#42416,#18275,#18276);
#14656=AXIS2_PLACEMENT_3D('',#42418,#18277,#18278);
#14657=AXIS2_PLACEMENT_3D('',#42420,#18279,#18280);
#14658=AXIS2_PLACEMENT_3D('',#42421,#18281,#18282);
#14659=AXIS2_PLACEMENT_3D('',#42530,#18283,#18284);
#14660=AXIS2_PLACEMENT_3D('',#42533,#18285,#18286);
#14661=AXIS2_PLACEMENT_3D('',#42542,#18287,#18288);
#14662=AXIS2_PLACEMENT_3D('',#42550,#18289,#18290);
#14663=AXIS2_PLACEMENT_3D('',#42552,#18291,#18292);
#14664=AXIS2_PLACEMENT_3D('',#42554,#18293,#18294);
#14665=AXIS2_PLACEMENT_3D('',#42564,#18295,#18296);
#14666=AXIS2_PLACEMENT_3D('',#42573,#18297,#18298);
#14667=AXIS2_PLACEMENT_3D('',#42575,#18299,#18300);
#14668=AXIS2_PLACEMENT_3D('',#42577,#18301,#18302);
#14669=AXIS2_PLACEMENT_3D('',#42578,#18303,#18304);
#14670=AXIS2_PLACEMENT_3D('',#42580,#18305,#18306);
#14671=AXIS2_PLACEMENT_3D('',#42582,#18307,#18308);
#14672=AXIS2_PLACEMENT_3D('',#42583,#18309,#18310);
#14673=AXIS2_PLACEMENT_3D('',#42692,#18311,#18312);
#14674=AXIS2_PLACEMENT_3D('',#42695,#18313,#18314);
#14675=AXIS2_PLACEMENT_3D('',#42704,#18315,#18316);
#14676=AXIS2_PLACEMENT_3D('',#42712,#18317,#18318);
#14677=AXIS2_PLACEMENT_3D('',#42714,#18319,#18320);
#14678=AXIS2_PLACEMENT_3D('',#42716,#18321,#18322);
#14679=AXIS2_PLACEMENT_3D('',#42726,#18323,#18324);
#14680=AXIS2_PLACEMENT_3D('',#42735,#18325,#18326);
#14681=AXIS2_PLACEMENT_3D('',#42737,#18327,#18328);
#14682=AXIS2_PLACEMENT_3D('',#42739,#18329,#18330);
#14683=AXIS2_PLACEMENT_3D('',#42740,#18331,#18332);
#14684=AXIS2_PLACEMENT_3D('',#42742,#18333,#18334);
#14685=AXIS2_PLACEMENT_3D('',#42744,#18335,#18336);
#14686=AXIS2_PLACEMENT_3D('',#42745,#18337,#18338);
#14687=AXIS2_PLACEMENT_3D('',#42854,#18339,#18340);
#14688=AXIS2_PLACEMENT_3D('',#42857,#18341,#18342);
#14689=AXIS2_PLACEMENT_3D('',#42866,#18343,#18344);
#14690=AXIS2_PLACEMENT_3D('',#42874,#18345,#18346);
#14691=AXIS2_PLACEMENT_3D('',#42876,#18347,#18348);
#14692=AXIS2_PLACEMENT_3D('',#42878,#18349,#18350);
#14693=AXIS2_PLACEMENT_3D('',#42888,#18351,#18352);
#14694=AXIS2_PLACEMENT_3D('',#42897,#18353,#18354);
#14695=AXIS2_PLACEMENT_3D('',#42899,#18355,#18356);
#14696=AXIS2_PLACEMENT_3D('',#42901,#18357,#18358);
#14697=AXIS2_PLACEMENT_3D('',#42902,#18359,#18360);
#14698=AXIS2_PLACEMENT_3D('',#42904,#18361,#18362);
#14699=AXIS2_PLACEMENT_3D('',#42906,#18363,#18364);
#14700=AXIS2_PLACEMENT_3D('',#42907,#18365,#18366);
#14701=AXIS2_PLACEMENT_3D('',#43016,#18367,#18368);
#14702=AXIS2_PLACEMENT_3D('',#43019,#18369,#18370);
#14703=AXIS2_PLACEMENT_3D('',#43028,#18371,#18372);
#14704=AXIS2_PLACEMENT_3D('',#43036,#18373,#18374);
#14705=AXIS2_PLACEMENT_3D('',#43038,#18375,#18376);
#14706=AXIS2_PLACEMENT_3D('',#43040,#18377,#18378);
#14707=AXIS2_PLACEMENT_3D('',#43050,#18379,#18380);
#14708=AXIS2_PLACEMENT_3D('',#43059,#18381,#18382);
#14709=AXIS2_PLACEMENT_3D('',#43061,#18383,#18384);
#14710=AXIS2_PLACEMENT_3D('',#43063,#18385,#18386);
#14711=AXIS2_PLACEMENT_3D('',#43064,#18387,#18388);
#14712=AXIS2_PLACEMENT_3D('',#43066,#18389,#18390);
#14713=AXIS2_PLACEMENT_3D('',#43068,#18391,#18392);
#14714=AXIS2_PLACEMENT_3D('',#43069,#18393,#18394);
#14715=AXIS2_PLACEMENT_3D('',#43178,#18395,#18396);
#14716=AXIS2_PLACEMENT_3D('',#43181,#18397,#18398);
#14717=AXIS2_PLACEMENT_3D('',#43190,#18399,#18400);
#14718=AXIS2_PLACEMENT_3D('',#43198,#18401,#18402);
#14719=AXIS2_PLACEMENT_3D('',#43200,#18403,#18404);
#14720=AXIS2_PLACEMENT_3D('',#43202,#18405,#18406);
#14721=AXIS2_PLACEMENT_3D('',#43212,#18407,#18408);
#14722=AXIS2_PLACEMENT_3D('',#43221,#18409,#18410);
#14723=AXIS2_PLACEMENT_3D('',#43223,#18411,#18412);
#14724=AXIS2_PLACEMENT_3D('',#43225,#18413,#18414);
#14725=AXIS2_PLACEMENT_3D('',#43226,#18415,#18416);
#14726=AXIS2_PLACEMENT_3D('',#43228,#18417,#18418);
#14727=AXIS2_PLACEMENT_3D('',#43230,#18419,#18420);
#14728=AXIS2_PLACEMENT_3D('',#43231,#18421,#18422);
#14729=AXIS2_PLACEMENT_3D('',#43340,#18423,#18424);
#14730=AXIS2_PLACEMENT_3D('',#43343,#18425,#18426);
#14731=AXIS2_PLACEMENT_3D('',#43345,#18427,#18428);
#14732=AXIS2_PLACEMENT_3D('',#43347,#18429,#18430);
#14733=AXIS2_PLACEMENT_3D('',#43357,#18431,#18432);
#14734=AXIS2_PLACEMENT_3D('',#43366,#18433,#18434);
#14735=AXIS2_PLACEMENT_3D('',#43368,#18435,#18436);
#14736=AXIS2_PLACEMENT_3D('',#43377,#18437,#18438);
#14737=AXIS2_PLACEMENT_3D('',#43385,#18439,#18440);
#14738=AXIS2_PLACEMENT_3D('',#43387,#18441,#18442);
#14739=AXIS2_PLACEMENT_3D('',#43388,#18443,#18444);
#14740=AXIS2_PLACEMENT_3D('',#43391,#18445,#18446);
#14741=AXIS2_PLACEMENT_3D('',#43400,#18447,#18448);
#14742=AXIS2_PLACEMENT_3D('',#43408,#18449,#18450);
#14743=AXIS2_PLACEMENT_3D('',#43410,#18451,#18452);
#14744=AXIS2_PLACEMENT_3D('',#43412,#18453,#18454);
#14745=AXIS2_PLACEMENT_3D('',#43422,#18455,#18456);
#14746=AXIS2_PLACEMENT_3D('',#43431,#18457,#18458);
#14747=AXIS2_PLACEMENT_3D('',#43433,#18459,#18460);
#14748=AXIS2_PLACEMENT_3D('',#43435,#18461,#18462);
#14749=AXIS2_PLACEMENT_3D('',#43436,#18463,#18464);
#14750=AXIS2_PLACEMENT_3D('',#43438,#18465,#18466);
#14751=AXIS2_PLACEMENT_3D('',#43440,#18467,#18468);
#14752=AXIS2_PLACEMENT_3D('',#43441,#18469,#18470);
#14753=AXIS2_PLACEMENT_3D('',#43550,#18471,#18472);
#14754=AXIS2_PLACEMENT_3D('',#43551,#18473,#18474);
#14755=AXIS2_PLACEMENT_3D('',#43552,#18475,#18476);
#14756=AXIS2_PLACEMENT_3D('',#43553,#18477,#18478);
#14757=AXIS2_PLACEMENT_3D('',#43554,#18479,#18480);
#14758=AXIS2_PLACEMENT_3D('',#43555,#18481,#18482);
#14759=AXIS2_PLACEMENT_3D('',#43556,#18483,#18484);
#14760=AXIS2_PLACEMENT_3D('',#43557,#18485,#18486);
#14761=AXIS2_PLACEMENT_3D('',#43558,#18487,#18488);
#14762=AXIS2_PLACEMENT_3D('',#43559,#18489,#18490);
#14763=AXIS2_PLACEMENT_3D('',#43560,#18491,#18492);
#14764=AXIS2_PLACEMENT_3D('',#43561,#18493,#18494);
#14765=AXIS2_PLACEMENT_3D('',#43562,#18495,#18496);
#14766=AXIS2_PLACEMENT_3D('',#43563,#18497,#18498);
#14767=AXIS2_PLACEMENT_3D('',#43564,#18499,#18500);
#14768=AXIS2_PLACEMENT_3D('',#43565,#18501,#18502);
#14769=AXIS2_PLACEMENT_3D('',#43566,#18503,#18504);
#14770=AXIS2_PLACEMENT_3D('',#43567,#18505,#18506);
#14771=AXIS2_PLACEMENT_3D('',#43568,#18507,#18508);
#14772=AXIS2_PLACEMENT_3D('',#43569,#18509,#18510);
#14773=AXIS2_PLACEMENT_3D('',#43570,#18511,#18512);
#14774=AXIS2_PLACEMENT_3D('',#43571,#18513,#18514);
#14775=AXIS2_PLACEMENT_3D('',#43572,#18515,#18516);
#14776=AXIS2_PLACEMENT_3D('',#43573,#18517,#18518);
#14777=AXIS2_PLACEMENT_3D('',#43574,#18519,#18520);
#14778=AXIS2_PLACEMENT_3D('',#43575,#18521,#18522);
#14779=AXIS2_PLACEMENT_3D('',#43576,#18523,#18524);
#14780=AXIS2_PLACEMENT_3D('',#43577,#18525,#18526);
#14781=AXIS2_PLACEMENT_3D('',#43578,#18527,#18528);
#14782=AXIS2_PLACEMENT_3D('',#43579,#18529,#18530);
#14783=AXIS2_PLACEMENT_3D('',#43580,#18531,#18532);
#14784=AXIS2_PLACEMENT_3D('',#43581,#18533,#18534);
#14785=AXIS2_PLACEMENT_3D('',#43582,#18535,#18536);
#14786=AXIS2_PLACEMENT_3D('',#43583,#18537,#18538);
#14787=AXIS2_PLACEMENT_3D('',#43584,#18539,#18540);
#14788=AXIS2_PLACEMENT_3D('',#43585,#18541,#18542);
#14789=AXIS2_PLACEMENT_3D('',#43586,#18543,#18544);
#14790=AXIS2_PLACEMENT_3D('',#43587,#18545,#18546);
#14791=AXIS2_PLACEMENT_3D('',#43588,#18547,#18548);
#14792=AXIS2_PLACEMENT_3D('',#43589,#18549,#18550);
#14793=AXIS2_PLACEMENT_3D('',#43590,#18551,#18552);
#14794=AXIS2_PLACEMENT_3D('',#43591,#18553,#18554);
#14795=AXIS2_PLACEMENT_3D('',#43592,#18555,#18556);
#14796=AXIS2_PLACEMENT_3D('',#43593,#18557,#18558);
#14797=AXIS2_PLACEMENT_3D('',#43594,#18559,#18560);
#14798=AXIS2_PLACEMENT_3D('',#43595,#18561,#18562);
#14799=AXIS2_PLACEMENT_3D('',#43596,#18563,#18564);
#14800=AXIS2_PLACEMENT_3D('',#43597,#18565,#18566);
#14801=AXIS2_PLACEMENT_3D('',#43598,#18567,#18568);
#14802=AXIS2_PLACEMENT_3D('',#43599,#18569,#18570);
#14803=AXIS2_PLACEMENT_3D('',#43600,#18571,#18572);
#14804=AXIS2_PLACEMENT_3D('',#43601,#18573,#18574);
#14805=AXIS2_PLACEMENT_3D('',#43602,#18575,#18576);
#14806=AXIS2_PLACEMENT_3D('',#43603,#18577,#18578);
#14807=AXIS2_PLACEMENT_3D('',#43604,#18579,#18580);
#14808=AXIS2_PLACEMENT_3D('',#43605,#18581,#18582);
#14809=AXIS2_PLACEMENT_3D('',#43606,#18583,#18584);
#14810=AXIS2_PLACEMENT_3D('',#43607,#18585,#18586);
#14811=AXIS2_PLACEMENT_3D('',#43608,#18587,#18588);
#14812=AXIS2_PLACEMENT_3D('',#43609,#18589,#18590);
#14813=AXIS2_PLACEMENT_3D('',#43610,#18591,#18592);
#14814=AXIS2_PLACEMENT_3D('',#43611,#18593,#18594);
#14815=AXIS2_PLACEMENT_3D('',#43612,#18595,#18596);
#14816=AXIS2_PLACEMENT_3D('',#43613,#18597,#18598);
#14817=AXIS2_PLACEMENT_3D('',#43614,#18599,#18600);
#14818=AXIS2_PLACEMENT_3D('',#43615,#18601,#18602);
#14819=AXIS2_PLACEMENT_3D('',#43616,#18603,#18604);
#14820=AXIS2_PLACEMENT_3D('',#43617,#18605,#18606);
#14821=AXIS2_PLACEMENT_3D('',#43618,#18607,#18608);
#14822=AXIS2_PLACEMENT_3D('',#43619,#18609,#18610);
#14823=AXIS2_PLACEMENT_3D('',#43620,#18611,#18612);
#14824=AXIS2_PLACEMENT_3D('',#43621,#18613,#18614);
#14825=AXIS2_PLACEMENT_3D('',#43622,#18615,#18616);
#14826=AXIS2_PLACEMENT_3D('',#43623,#18617,#18618);
#14827=AXIS2_PLACEMENT_3D('',#43624,#18619,#18620);
#14828=AXIS2_PLACEMENT_3D('',#43625,#18621,#18622);
#14829=AXIS2_PLACEMENT_3D('',#43626,#18623,#18624);
#14830=AXIS2_PLACEMENT_3D('',#43627,#18625,#18626);
#14831=AXIS2_PLACEMENT_3D('',#43628,#18627,#18628);
#14832=AXIS2_PLACEMENT_3D('',#43629,#18629,#18630);
#14833=AXIS2_PLACEMENT_3D('',#43630,#18631,#18632);
#14834=AXIS2_PLACEMENT_3D('',#43631,#18633,#18634);
#14835=AXIS2_PLACEMENT_3D('',#43632,#18635,#18636);
#14836=AXIS2_PLACEMENT_3D('',#43633,#18637,#18638);
#14837=AXIS2_PLACEMENT_3D('',#43634,#18639,#18640);
#14838=AXIS2_PLACEMENT_3D('',#43635,#18641,#18642);
#14839=AXIS2_PLACEMENT_3D('',#43636,#18643,#18644);
#14840=AXIS2_PLACEMENT_3D('',#43637,#18645,#18646);
#14841=AXIS2_PLACEMENT_3D('',#43638,#18647,#18648);
#14842=AXIS2_PLACEMENT_3D('',#43639,#18649,#18650);
#14843=AXIS2_PLACEMENT_3D('',#43640,#18651,#18652);
#14844=AXIS2_PLACEMENT_3D('',#43641,#18653,#18654);
#14845=AXIS2_PLACEMENT_3D('',#43642,#18655,#18656);
#14846=AXIS2_PLACEMENT_3D('',#43643,#18657,#18658);
#14847=AXIS2_PLACEMENT_3D('',#43644,#18659,#18660);
#14848=AXIS2_PLACEMENT_3D('',#43645,#18661,#18662);
#14849=AXIS2_PLACEMENT_3D('',#43646,#18663,#18664);
#14850=AXIS2_PLACEMENT_3D('',#43647,#18665,#18666);
#14851=AXIS2_PLACEMENT_3D('',#43648,#18667,#18668);
#14852=AXIS2_PLACEMENT_3D('',#43649,#18669,#18670);
#14853=AXIS2_PLACEMENT_3D('',#43650,#18671,#18672);
#14854=AXIS2_PLACEMENT_3D('',#43651,#18673,#18674);
#14855=AXIS2_PLACEMENT_3D('',#43652,#18675,#18676);
#14856=AXIS2_PLACEMENT_3D('',#43653,#18677,#18678);
#14857=AXIS2_PLACEMENT_3D('',#43654,#18679,#18680);
#14858=AXIS2_PLACEMENT_3D('',#43655,#18681,#18682);
#14859=AXIS2_PLACEMENT_3D('',#43656,#18683,#18684);
#14860=AXIS2_PLACEMENT_3D('',#43657,#18685,#18686);
#14861=AXIS2_PLACEMENT_3D('',#43658,#18687,#18688);
#14862=AXIS2_PLACEMENT_3D('',#43659,#18689,#18690);
#14863=AXIS2_PLACEMENT_3D('',#43660,#18691,#18692);
#14864=AXIS2_PLACEMENT_3D('',#43661,#18693,#18694);
#14865=AXIS2_PLACEMENT_3D('',#43662,#18695,#18696);
#14866=AXIS2_PLACEMENT_3D('',#43663,#18697,#18698);
#14867=AXIS2_PLACEMENT_3D('',#43664,#18699,#18700);
#14868=AXIS2_PLACEMENT_3D('',#43665,#18701,#18702);
#14869=AXIS2_PLACEMENT_3D('',#43666,#18703,#18704);
#14870=AXIS2_PLACEMENT_3D('',#43667,#18705,#18706);
#14871=AXIS2_PLACEMENT_3D('',#43668,#18707,#18708);
#14872=AXIS2_PLACEMENT_3D('',#43669,#18709,#18710);
#14873=AXIS2_PLACEMENT_3D('',#43670,#18711,#18712);
#14874=AXIS2_PLACEMENT_3D('',#43671,#18713,#18714);
#14875=AXIS2_PLACEMENT_3D('',#43672,#18715,#18716);
#14876=AXIS2_PLACEMENT_3D('',#43673,#18717,#18718);
#14877=AXIS2_PLACEMENT_3D('',#43674,#18719,#18720);
#14878=AXIS2_PLACEMENT_3D('',#43675,#18721,#18722);
#18083=DIRECTION('axis',(0.,0.,1.));
#18084=DIRECTION('refdir',(1.,0.,0.));
#18085=DIRECTION('center_axis',(0.,-1.83697019872103E-16,-1.));
#18086=DIRECTION('ref_axis',(0.,-1.,1.83697019872103E-16));
#18087=DIRECTION('center_axis',(0.,1.83697019872103E-16,1.));
#18088=DIRECTION('ref_axis',(0.,-1.,1.83697019872103E-16));
#18089=DIRECTION('center_axis',(-1.,1.22464679914735E-16,-2.24963967399279E-32));
#18090=DIRECTION('ref_axis',(1.22464679914735E-16,1.,-1.83697019872103E-16));
#18091=DIRECTION('center_axis',(0.,1.83697019872103E-16,1.));
#18092=DIRECTION('ref_axis',(0.,-1.,1.83697019872103E-16));
#18093=DIRECTION('center_axis',(0.,1.83697019872103E-16,1.));
#18094=DIRECTION('ref_axis',(0.,1.,-2.09599627067876E-16));
#18095=DIRECTION('center_axis',(0.,-1.83697019872103E-16,-1.));
#18096=DIRECTION('ref_axis',(0.,1.,-1.83697019872103E-16));
#18097=DIRECTION('center_axis',(1.,1.22464679914735E-16,-2.24963967399279E-32));
#18098=DIRECTION('ref_axis',(1.22464679914735E-16,-1.,1.30999766917423E-16));
#18099=DIRECTION('center_axis',(0.,1.83697019872103E-16,1.));
#18100=DIRECTION('ref_axis',(0.,1.,-1.83697019872103E-16));
#18101=DIRECTION('center_axis',(0.,1.83697019872103E-16,1.));
#18102=DIRECTION('ref_axis',(0.,1.,-1.83697019872103E-16));
#18103=DIRECTION('center_axis',(0.,-1.83697019872103E-16,-1.));
#18104=DIRECTION('ref_axis',(0.,1.,-1.83697019872103E-16));
#18105=DIRECTION('center_axis',(0.,1.83697019872103E-16,1.));
#18106=DIRECTION('ref_axis',(0.,1.,-2.09599627067876E-16));
#18107=DIRECTION('center_axis',(0.,-1.83697019872103E-16,-1.));
#18108=DIRECTION('ref_axis',(0.,1.,-1.83697019872103E-16));
#18109=DIRECTION('center_axis',(1.,1.22464679914735E-16,-2.24963967399279E-32));
#18110=DIRECTION('ref_axis',(1.22464679914735E-16,-1.,1.30999766917423E-16));
#18111=DIRECTION('center_axis',(0.,1.83697019872103E-16,1.));
#18112=DIRECTION('ref_axis',(0.,-1.,1.83697019872103E-16));
#18113=DIRECTION('center_axis',(0.,-1.83697019872103E-16,-1.));
#18114=DIRECTION('ref_axis',(0.,1.,-1.83697019872103E-16));
#18115=DIRECTION('center_axis',(0.,-1.83697019872103E-16,-1.));
#18116=DIRECTION('ref_axis',(0.,-1.,1.83697019872103E-16));
#18117=DIRECTION('',(8.65956056235483E-17,0.707106781186539,-0.707106781186556));
#18118=DIRECTION('center_axis',(0.,1.83697019872103E-16,1.));
#18119=DIRECTION('ref_axis',(0.,-1.,1.83697019872103E-16));
#18120=DIRECTION('center_axis',(0.,1.83697019872103E-16,1.));
#18121=DIRECTION('ref_axis',(0.,-1.,1.83697019872103E-16));
#18122=DIRECTION('',(0.,1.83697019872103E-16,1.));
#18123=DIRECTION('center_axis',(0.,1.83697019872103E-16,1.));
#18124=DIRECTION('ref_axis',(0.,1.,-1.83697019872103E-16));
#18125=DIRECTION('',(8.65956056235483E-17,-0.707106781186539,0.707106781186556));
#18126=DIRECTION('center_axis',(0.,1.83697019872103E-16,1.));
#18127=DIRECTION('ref_axis',(0.,-1.,1.83697019872103E-16));
#18128=DIRECTION('center_axis',(0.,1.83697019872103E-16,1.));
#18129=DIRECTION('ref_axis',(0.,-1.,1.83697019872103E-16));
#18130=DIRECTION('center_axis',(0.,1.83697019872103E-16,1.));
#18131=DIRECTION('ref_axis',(0.,-1.,1.83697019872103E-16));
#18132=DIRECTION('',(0.,-1.83697019872103E-16,-1.));
#18133=DIRECTION('center_axis',(0.,1.83697019872103E-16,1.));
#18134=DIRECTION('ref_axis',(0.,-1.,1.83697019872103E-16));
#18135=DIRECTION('',(0.,-1.83697019872103E-16,-1.));
#18136=DIRECTION('center_axis',(0.,1.83697019872103E-16,1.));
#18137=DIRECTION('ref_axis',(0.,-1.,1.83697019872103E-16));
#18138=DIRECTION('center_axis',(0.,-1.83697019872103E-16,-1.));
#18139=DIRECTION('ref_axis',(0.,1.,-1.83697019872103E-16));
#18140=DIRECTION('center_axis',(0.,1.83697019872103E-16,1.));
#18141=DIRECTION('ref_axis',(0.,-1.,1.83697019872103E-16));
#18142=DIRECTION('center_axis',(-1.,0.,0.));
#18143=DIRECTION('ref_axis',(0.,1.,0.));
#18144=DIRECTION('center_axis',(0.,1.22464679914735E-16,1.));
#18145=DIRECTION('ref_axis',(0.,-1.,1.22464679914735E-16));
#18146=DIRECTION('center_axis',(-0.623489801858732,0.781831482468031,-1.43620113371566E-16));
#18147=DIRECTION('ref_axis',(0.781831482468031,0.623489801858732,6.91638013500061E-17));
#18148=DIRECTION('center_axis',(-4.78733711238555E-17,1.45519280364738E-16,
1.));
#18149=DIRECTION('ref_axis',(-0.781831482468031,-0.623489801858732,5.33008785647293E-17));
#18150=DIRECTION('center_axis',(0.222520933956319,0.974927912181823,-1.79091352057932E-16));
#18151=DIRECTION('ref_axis',(0.974927912181823,-0.222520933956319,2.24573452299036E-16));
#18152=DIRECTION('center_axis',(-5.96971173526444E-17,1.97322497347747E-16,
1.));
#18153=DIRECTION('ref_axis',(-0.974927912181823,0.222520933956319,-1.02108772384301E-16));
#18154=DIRECTION('center_axis',(0.900968867902422,0.433883739117552,-7.97031498468594E-17));
#18155=DIRECTION('ref_axis',(0.433883739117552,-0.900968867902422,3.4920231590332E-16));
#18156=DIRECTION('center_axis',(-2.65677166156194E-17,2.38865451882509E-16,
1.));
#18157=DIRECTION('ref_axis',(-0.433883739117552,0.900968867902422,-2.26737635988585E-16));
#18158=DIRECTION('center_axis',(0.900968867902416,-0.433883739117565,7.97031498468616E-17));
#18159=DIRECTION('ref_axis',(-0.433883739117565,-0.900968867902416,3.49202315903319E-16));
#18160=DIRECTION('center_axis',(2.65677166156204E-17,2.38865451882508E-16,
1.));
#18161=DIRECTION('ref_axis',(0.433883739117565,0.900968867902416,-2.26737635988584E-16));
#18162=DIRECTION('center_axis',(0.222520933956305,-0.974927912181826,1.79091352057933E-16));
#18163=DIRECTION('ref_axis',(-0.974927912181826,-0.222520933956305,2.24573452299033E-16));
#18164=DIRECTION('center_axis',(5.9697117352644E-17,1.97322497347747E-16,
1.));
#18165=DIRECTION('ref_axis',(0.974927912181826,0.222520933956305,-1.02108772384298E-16));
#18166=DIRECTION('center_axis',(-0.623489801858743,-0.781831482468022,1.43620113371564E-16));
#18167=DIRECTION('ref_axis',(-0.781831482468022,0.623489801858743,6.91638013500039E-17));
#18168=DIRECTION('center_axis',(4.78733711238546E-17,1.45519280364737E-16,
1.));
#18169=DIRECTION('ref_axis',(0.781831482468022,-0.623489801858743,5.33008785647315E-17));
#18170=DIRECTION('center_axis',(0.,1.83697019872103E-16,1.));
#18171=DIRECTION('ref_axis',(0.,1.,-1.62614292875575E-16));
#18172=DIRECTION('center_axis',(0.,-1.83697019872103E-16,-1.));
#18173=DIRECTION('ref_axis',(0.,1.,-1.83697019872103E-16));
#18174=DIRECTION('center_axis',(1.,1.22464679914735E-16,-2.24963967399279E-32));
#18175=DIRECTION('ref_axis',(1.22464679914735E-16,-1.,2.03267866094469E-16));
#18176=DIRECTION('center_axis',(0.,1.83697019872103E-16,1.));
#18177=DIRECTION('ref_axis',(0.,1.,-1.83697019872103E-16));
#18178=DIRECTION('center_axis',(0.,1.83697019872103E-16,1.));
#18179=DIRECTION('ref_axis',(0.,1.,-1.83697019872103E-16));
#18180=DIRECTION('center_axis',(0.,-1.83697019872103E-16,-1.));
#18181=DIRECTION('ref_axis',(0.,-1.,1.64970202400831E-16));
#18182=DIRECTION('center_axis',(0.,1.83697019872103E-16,1.));
#18183=DIRECTION('ref_axis',(0.,-1.,1.83697019872103E-16));
#18184=DIRECTION('center_axis',(1.,-1.22464679914735E-16,2.24963967399279E-32));
#18185=DIRECTION('ref_axis',(1.22464679914735E-16,1.,-2.06212753001039E-16));
#18186=DIRECTION('center_axis',(0.,-1.83697019872103E-16,-1.));
#18187=DIRECTION('ref_axis',(0.,-1.,1.83697019872103E-16));
#18188=DIRECTION('center_axis',(0.,-1.83697019872103E-16,-1.));
#18189=DIRECTION('ref_axis',(0.,-1.,1.62614292875575E-16));
#18190=DIRECTION('center_axis',(0.,1.83697019872103E-16,1.));
#18191=DIRECTION('ref_axis',(0.,-1.,1.83697019872103E-16));
#18192=DIRECTION('center_axis',(1.,-1.22464679914735E-16,2.24963967399279E-32));
#18193=DIRECTION('ref_axis',(1.22464679914735E-16,1.,-2.03267866094469E-16));
#18194=DIRECTION('center_axis',(0.,-1.83697019872103E-16,-1.));
#18195=DIRECTION('ref_axis',(0.,-1.,1.83697019872103E-16));
#18196=DIRECTION('center_axis',(0.,1.83697019872103E-16,1.));
#18197=DIRECTION('ref_axis',(0.,1.,-1.64970202400831E-16));
#18198=DIRECTION('center_axis',(0.,-1.83697019872103E-16,-1.));
#18199=DIRECTION('ref_axis',(0.,1.,-1.83697019872103E-16));
#18200=DIRECTION('center_axis',(1.,1.22464679914735E-16,-2.24963967399279E-32));
#18201=DIRECTION('ref_axis',(1.22464679914735E-16,-1.,2.06212753001039E-16));
#18202=DIRECTION('center_axis',(0.,1.83697019872103E-16,1.));
#18203=DIRECTION('ref_axis',(0.,1.,-1.83697019872103E-16));
#18204=DIRECTION('center_axis',(0.,-1.83697019872103E-16,-1.));
#18205=DIRECTION('ref_axis',(0.,1.,-1.83697019872103E-16));
#18206=DIRECTION('center_axis',(0.,1.83697019872103E-16,1.));
#18207=DIRECTION('ref_axis',(0.,-1.,1.83697019872103E-16));
#18208=DIRECTION('center_axis',(0.,1.83697019872103E-16,1.));
#18209=DIRECTION('ref_axis',(0.,-1.,1.83697019872103E-16));
#18210=DIRECTION('',(0.,1.83697019872103E-16,1.));
#18211=DIRECTION('center_axis',(0.,1.83697019872103E-16,1.));
#18212=DIRECTION('ref_axis',(0.,-1.,1.83697019872103E-16));
#18213=DIRECTION('center_axis',(0.,1.83697019872103E-16,1.));
#18214=DIRECTION('ref_axis',(0.,-1.,1.83697019872103E-16));
#18215=DIRECTION('',(0.,1.83697019872103E-16,1.));
#18216=DIRECTION('center_axis',(0.,1.83697019872103E-16,1.));
#18217=DIRECTION('ref_axis',(0.,-1.,1.83697019872103E-16));
#18218=DIRECTION('center_axis',(0.,1.83697019872103E-16,1.));
#18219=DIRECTION('ref_axis',(0.,-1.,1.83697019872103E-16));
#18220=DIRECTION('center_axis',(0.,1.83697019872103E-16,1.));
#18221=DIRECTION('ref_axis',(0.,-1.,1.83697019872103E-16));
#18222=DIRECTION('',(0.,1.83697019872103E-16,1.));
#18223=DIRECTION('center_axis',(0.,-1.83697019872103E-16,-1.));
#18224=DIRECTION('ref_axis',(0.,-1.,1.83697019872103E-16));
#18225=DIRECTION('center_axis',(-1.,1.22464679914735E-16,-2.24963967399279E-32));
#18226=DIRECTION('ref_axis',(1.22464679914735E-16,1.,-1.83697019872103E-16));
#18227=DIRECTION('center_axis',(0.,1.83697019872103E-16,1.));
#18228=DIRECTION('ref_axis',(0.,-1.,1.83697019872103E-16));
#18229=DIRECTION('center_axis',(0.,1.83697019872103E-16,1.));
#18230=DIRECTION('ref_axis',(0.,-1.,1.83697019872103E-16));
#18231=DIRECTION('',(0.,1.83697019872103E-16,1.));
#18232=DIRECTION('center_axis',(0.,1.83697019872103E-16,1.));
#18233=DIRECTION('ref_axis',(0.,-1.,1.83697019872103E-16));
#18234=DIRECTION('center_axis',(0.,1.83697019872103E-16,1.));
#18235=DIRECTION('ref_axis',(0.,-1.,1.83697019872103E-16));
#18236=DIRECTION('',(0.,1.83697019872103E-16,1.));
#18237=DIRECTION('center_axis',(0.,1.83697019872103E-16,1.));
#18238=DIRECTION('ref_axis',(0.,-1.,1.83697019872103E-16));
#18239=DIRECTION('center_axis',(0.,1.83697019872103E-16,1.));
#18240=DIRECTION('ref_axis',(0.,-1.,1.83697019872103E-16));
#18241=DIRECTION('',(0.,1.83697019872103E-16,1.));
#18242=DIRECTION('center_axis',(0.,1.83697019872103E-16,1.));
#18243=DIRECTION('ref_axis',(0.,-1.,1.83697019872103E-16));
#18244=DIRECTION('center_axis',(0.,-1.83697019872103E-16,-1.));
#18245=DIRECTION('ref_axis',(0.,-1.,1.83697019872103E-16));
#18246=DIRECTION('center_axis',(0.,1.83697019872103E-16,1.));
#18247=DIRECTION('ref_axis',(0.,-1.,1.83697019872103E-16));
#18248=DIRECTION('',(-8.65956056235488E-17,-0.707106781186543,0.707106781186552));
#18249=DIRECTION('center_axis',(0.,1.83697019872103E-16,1.));
#18250=DIRECTION('ref_axis',(0.,-1.,1.83697019872103E-16));
#18251=DIRECTION('center_axis',(0.,1.83697019872103E-16,1.));
#18252=DIRECTION('ref_axis',(0.,1.,-1.83697019872103E-16));
#18253=DIRECTION('center_axis',(0.,1.83697019872103E-16,1.));
#18254=DIRECTION('ref_axis',(0.,-1.,1.83697019872103E-16));
#18255=DIRECTION('center_axis',(0.,1.83697019872103E-16,1.));
#18256=DIRECTION('ref_axis',(0.,-1.,1.83697019872103E-16));
#18257=DIRECTION('',(-8.65956056235488E-17,0.707106781186543,-0.707106781186552));
#18258=DIRECTION('center_axis',(0.,1.83697019872103E-16,1.));
#18259=DIRECTION('ref_axis',(0.,-1.,1.83697019872103E-16));
#18260=DIRECTION('center_axis',(0.,1.83697019872103E-16,1.));
#18261=DIRECTION('ref_axis',(0.,-1.,1.83697019872103E-16));
#18262=DIRECTION('',(0.,-1.83697019872103E-16,-1.));
#18263=DIRECTION('center_axis',(0.,-1.83697019872103E-16,-1.));
#18264=DIRECTION('ref_axis',(0.,1.,-1.83697019872103E-16));
#18265=DIRECTION('center_axis',(0.,1.83697019872103E-16,1.));
#18266=DIRECTION('ref_axis',(0.,-1.,1.83697019872103E-16));
#18267=DIRECTION('center_axis',(0.,-1.83697019872103E-16,-1.));
#18268=DIRECTION('ref_axis',(0.,1.,-1.83697019872103E-16));
#18269=DIRECTION('center_axis',(0.,1.83697019872103E-16,1.));
#18270=DIRECTION('ref_axis',(0.,-1.,1.83697019872103E-16));
#18271=DIRECTION('center_axis',(0.,-1.83697019872103E-16,-1.));
#18272=DIRECTION('ref_axis',(0.,1.,-1.83697019872103E-16));
#18273=DIRECTION('center_axis',(0.,1.83697019872103E-16,1.));
#18274=DIRECTION('ref_axis',(0.,-1.,1.83697019872103E-16));
#18275=DIRECTION('center_axis',(-0.781831482468031,0.623489801858732,6.91638013500059E-17));
#18276=DIRECTION('ref_axis',(0.,0.,-1.));
#18277=DIRECTION('center_axis',(0.781831482468031,-0.623489801858732,-6.91638013500059E-17));
#18278=DIRECTION('ref_axis',(-5.40744373425995E-17,4.31229247995119E-17,
-1.));
#18279=DIRECTION('center_axis',(0.623489801858732,0.781831482468031,0.));
#18280=DIRECTION('ref_axis',(0.,0.,1.));
#18281=DIRECTION('center_axis',(0.781831482468031,-0.623489801858732,-6.91638013500059E-17));
#18282=DIRECTION('ref_axis',(-5.40744373425995E-17,4.31229247995119E-17,
-1.));
#18283=DIRECTION('center_axis',(0.623489801858732,0.781831482468031,-1.22464679914735E-16));
#18284=DIRECTION('ref_axis',(0.,0.,-1.));
#18285=DIRECTION('center_axis',(1.79091352057932E-16,2.24573452299036E-16,
1.));
#18286=DIRECTION('ref_axis',(-5.50003967499518E-33,-1.,2.24573452299036E-16));
#18287=DIRECTION('center_axis',(1.79091352057932E-16,2.24573452299036E-16,
1.));
#18288=DIRECTION('ref_axis',(-5.5000396749952E-33,-1.,2.24573452299036E-16));
#18289=DIRECTION('center_axis',(1.79091352057932E-16,2.24573452299036E-16,
1.));
#18290=DIRECTION('ref_axis',(-5.50003967499518E-33,-1.,2.24573452299036E-16));
#18291=DIRECTION('center_axis',(-0.781831482468031,0.623489801858732,0.));
#18292=DIRECTION('ref_axis',(0.,0.,1.));
#18293=DIRECTION('center_axis',(1.43620113371566E-16,6.91638013500059E-17,
1.));
#18294=DIRECTION('ref_axis',(0.623489801858732,0.781831482468031,-1.43620113371566E-16));
#18295=DIRECTION('center_axis',(1.43620113371566E-16,6.91638013500059E-17,
1.));
#18296=DIRECTION('ref_axis',(0.623489801858732,0.781831482468031,-1.43620113371566E-16));
#18297=DIRECTION('center_axis',(1.43620113371566E-16,6.91638013500059E-17,
1.));
#18298=DIRECTION('ref_axis',(0.623489801858732,0.781831482468031,-1.43620113371566E-16));
#18299=DIRECTION('center_axis',(0.781831482468031,-0.623489801858732,-6.91638013500059E-17));
#18300=DIRECTION('ref_axis',(-5.40744373425995E-17,4.31229247995119E-17,
-1.));
#18301=DIRECTION('center_axis',(0.781831482468031,-0.623489801858732,-6.91638013500059E-17));
#18302=DIRECTION('ref_axis',(-5.40744373425995E-17,4.31229247995119E-17,
-1.));
#18303=DIRECTION('center_axis',(-0.974927912181823,-0.222520933956318,2.24573452299036E-16));
#18304=DIRECTION('ref_axis',(0.,-2.10741377257197E-16,-1.));
#18305=DIRECTION('center_axis',(0.974927912181823,0.222520933956318,-2.24573452299036E-16));
#18306=DIRECTION('ref_axis',(-1.71433215598957E-16,-2.58125940401653E-16,
-1.));
#18307=DIRECTION('center_axis',(-0.222520933956318,0.974927912181823,-3.85233095511903E-16));
#18308=DIRECTION('ref_axis',(0.,3.95140082357245E-16,1.));
#18309=DIRECTION('center_axis',(0.974927912181823,0.222520933956318,-2.24573452299036E-16));
#18310=DIRECTION('ref_axis',(-1.71433215598957E-16,-2.58125940401653E-16,
-1.));
#18311=DIRECTION('center_axis',(-0.222520933956318,0.974927912181823,-3.59586625308286E-16));
#18312=DIRECTION('ref_axis',(0.,-2.4905725751517E-16,-1.));
#18313=DIRECTION('center_axis',(7.97031498468594E-17,3.4920231590332E-16,
1.));
#18314=DIRECTION('ref_axis',(2.39882519785021E-33,-1.,3.4920231590332E-16));
#18315=DIRECTION('center_axis',(7.97031498468594E-17,3.4920231590332E-16,
1.));
#18316=DIRECTION('ref_axis',(2.39882519785021E-33,-1.,3.4920231590332E-16));
#18317=DIRECTION('center_axis',(7.97031498468594E-17,3.4920231590332E-16,
1.));
#18318=DIRECTION('ref_axis',(2.39882519785021E-33,-1.,3.4920231590332E-16));
#18319=DIRECTION('center_axis',(-0.974927912181823,-0.222520933956318,6.92755669385935E-17));
#18320=DIRECTION('ref_axis',(0.,3.11321571893962E-16,1.));
#18321=DIRECTION('center_axis',(1.79091352057932E-16,2.24573452299036E-16,
1.));
#18322=DIRECTION('ref_axis',(-0.222520933956318,0.974927912181823,-1.79091352057933E-16));
#18323=DIRECTION('center_axis',(1.79091352057932E-16,2.24573452299036E-16,
1.));
#18324=DIRECTION('ref_axis',(-0.222520933956318,0.974927912181823,-1.79091352057933E-16));
#18325=DIRECTION('center_axis',(1.79091352057932E-16,2.24573452299036E-16,
1.));
#18326=DIRECTION('ref_axis',(-0.222520933956318,0.974927912181823,-1.79091352057933E-16));
#18327=DIRECTION('center_axis',(0.974927912181823,0.222520933956318,-2.24573452299036E-16));
#18328=DIRECTION('ref_axis',(-1.64444757441796E-16,-2.88744376156862E-16,
-1.));
#18329=DIRECTION('center_axis',(0.974927912181823,0.222520933956318,-2.24573452299036E-16));
#18330=DIRECTION('ref_axis',(-1.64444757441796E-16,-2.88744376156862E-16,
-1.));
#18331=DIRECTION('center_axis',(-0.433883739117553,-0.900968867902422,3.4920231590332E-16));
#18332=DIRECTION('ref_axis',(0.,-4.21482754514395E-16,-1.));
#18333=DIRECTION('center_axis',(0.433883739117553,0.900968867902422,-3.4920231590332E-16));
#18334=DIRECTION('ref_axis',(1.97058769816641E-17,-3.97075180104293E-16,
-1.));
#18335=DIRECTION('center_axis',(-0.900968867902422,0.433883739117553,-2.28593141877839E-16));
#18336=DIRECTION('ref_axis',(0.,5.26853443142994E-16,1.));
#18337=DIRECTION('center_axis',(0.433883739117553,0.900968867902422,-3.4920231590332E-16));
#18338=DIRECTION('ref_axis',(1.97058769816641E-17,-3.97075180104293E-16,
-1.));
#18339=DIRECTION('center_axis',(-0.900968867902422,0.433883739117552,-3.33523066916777E-16));
#18340=DIRECTION('ref_axis',(0.,-4.9811451503034E-16,-1.));
#18341=DIRECTION('center_axis',(-7.97031498468617E-17,3.49202315903319E-16,
1.));
#18342=DIRECTION('ref_axis',(-2.39882519785018E-33,-1.,3.49202315903319E-16));
#18343=DIRECTION('center_axis',(-7.97031498468617E-17,3.49202315903319E-16,
1.));
#18344=DIRECTION('ref_axis',(-2.39882519785018E-33,-1.,3.49202315903319E-16));
#18345=DIRECTION('center_axis',(-7.97031498468617E-17,3.49202315903319E-16,
1.));
#18346=DIRECTION('ref_axis',(-2.39882519785018E-33,-1.,3.49202315903319E-16));
#18347=DIRECTION('center_axis',(-0.433883739117552,-0.900968867902422,5.60982088365811E-16));
#18348=DIRECTION('ref_axis',(0.,6.22643143787925E-16,1.));
#18349=DIRECTION('center_axis',(7.97031498468594E-17,3.4920231590332E-16,
1.));
#18350=DIRECTION('ref_axis',(-0.900968867902422,0.433883739117553,-7.97031498468594E-17));
#18351=DIRECTION('center_axis',(7.97031498468594E-17,3.4920231590332E-16,
1.));
#18352=DIRECTION('ref_axis',(-0.900968867902422,0.433883739117553,-7.97031498468594E-17));
#18353=DIRECTION('center_axis',(7.97031498468594E-17,3.4920231590332E-16,
1.));
#18354=DIRECTION('ref_axis',(-0.900968867902422,0.433883739117553,-7.97031498468594E-17));
#18355=DIRECTION('center_axis',(0.433883739117553,0.900968867902422,-3.4920231590332E-16));
#18356=DIRECTION('ref_axis',(4.4891409918625E-17,-4.09203893527874E-16,
-1.));
#18357=DIRECTION('center_axis',(0.433883739117553,0.900968867902422,-3.4920231590332E-16));
#18358=DIRECTION('ref_axis',(4.48914099186251E-17,-4.09203893527874E-16,
-1.));
#18359=DIRECTION('center_axis',(0.433883739117565,-0.900968867902416,3.49202315903319E-16));
#18360=DIRECTION('ref_axis',(0.,-4.21482754514395E-16,-1.));
#18361=DIRECTION('center_axis',(-0.433883739117565,0.900968867902416,-3.49202315903319E-16));
#18362=DIRECTION('ref_axis',(-1.97058769816642E-17,-3.97075180104295E-16,
-1.));
#18363=DIRECTION('center_axis',(-0.900968867902416,-0.433883739117565,2.28593141877845E-16));
#18364=DIRECTION('ref_axis',(0.,5.26853443142994E-16,1.));
#18365=DIRECTION('center_axis',(-0.433883739117565,0.900968867902416,-3.49202315903319E-16));
#18366=DIRECTION('ref_axis',(-1.97058769816642E-17,-3.97075180104295E-16,
-1.));
#18367=DIRECTION('center_axis',(-0.900968867902416,-0.433883739117565,8.85937070873124E-17));
#18368=DIRECTION('ref_axis',(0.,-4.9811451503034E-16,-1.));
#18369=DIRECTION('center_axis',(-1.79091352057933E-16,2.24573452299033E-16,
1.));
#18370=DIRECTION('ref_axis',(5.50003967499563E-33,-1.,2.24573452299033E-16));
#18371=DIRECTION('center_axis',(-1.79091352057933E-16,2.24573452299033E-16,
1.));
#18372=DIRECTION('ref_axis',(5.50003967499563E-33,-1.,2.24573452299033E-16));
#18373=DIRECTION('center_axis',(-1.79091352057933E-16,2.24573452299033E-16,
1.));
#18374=DIRECTION('ref_axis',(5.50003967499563E-33,-1.,2.24573452299033E-16));
#18375=DIRECTION('center_axis',(0.433883739117565,-0.900968867902416,5.60982088365808E-16));
#18376=DIRECTION('ref_axis',(0.,6.22643143787925E-16,1.));
#18377=DIRECTION('center_axis',(-7.97031498468617E-17,3.49202315903319E-16,
1.));
#18378=DIRECTION('ref_axis',(-0.900968867902416,-0.433883739117565,7.97031498468616E-17));
#18379=DIRECTION('center_axis',(-7.97031498468617E-17,3.49202315903319E-16,
1.));
#18380=DIRECTION('ref_axis',(-0.900968867902416,-0.433883739117565,7.97031498468616E-17));
#18381=DIRECTION('center_axis',(-7.97031498468617E-17,3.49202315903319E-16,
1.));
#18382=DIRECTION('ref_axis',(-0.900968867902416,-0.433883739117565,7.97031498468616E-17));
#18383=DIRECTION('center_axis',(-0.433883739117565,0.900968867902416,-3.49202315903319E-16));
#18384=DIRECTION('ref_axis',(-4.48914099186257E-17,-4.09203893527877E-16,
-1.));
#18385=DIRECTION('center_axis',(-0.433883739117565,0.900968867902416,-3.49202315903319E-16));
#18386=DIRECTION('ref_axis',(-4.48914099186258E-17,-4.09203893527877E-16,
-1.));
#18387=DIRECTION('center_axis',(0.974927912181826,-0.222520933956305,2.24573452299033E-16));
#18388=DIRECTION('ref_axis',(0.,-2.10741377257197E-16,-1.));
#18389=DIRECTION('center_axis',(-0.974927912181826,0.222520933956305,-2.24573452299033E-16));
#18390=DIRECTION('ref_axis',(1.71433215598957E-16,-2.58125940401651E-16,
-1.));
#18391=DIRECTION('center_axis',(-0.222520933956305,-0.974927912181826,1.28411031837301E-16));
#18392=DIRECTION('ref_axis',(0.,1.31713360785748E-16,1.));
#18393=DIRECTION('center_axis',(-0.974927912181826,0.222520933956305,-2.24573452299033E-16));
#18394=DIRECTION('ref_axis',(1.71433215598957E-16,-2.58125940401651E-16,
-1.));
#18395=DIRECTION('center_axis',(-0.222520933956305,-0.974927912181826,1.14657265478815E-16));
#18396=DIRECTION('ref_axis',(0.,-1.24528628757585E-16,-1.));
#18397=DIRECTION('center_axis',(-1.43620113371564E-16,6.91638013500039E-17,
1.));
#18398=DIRECTION('ref_axis',(1.,1.10509814492259E-33,1.43620113371564E-16));
#18399=DIRECTION('center_axis',(-1.43620113371564E-16,6.91638013500039E-17,
1.));
#18400=DIRECTION('ref_axis',(1.,1.10509814492259E-33,1.43620113371564E-16));
#18401=DIRECTION('center_axis',(-1.43620113371564E-16,6.91638013500039E-17,
1.));
#18402=DIRECTION('ref_axis',(1.,1.10509814492259E-33,1.43620113371564E-16));
#18403=DIRECTION('center_axis',(0.974927912181826,-0.222520933956305,3.46377834692947E-17));
#18404=DIRECTION('ref_axis',(0.,1.55660785946981E-16,1.));
#18405=DIRECTION('center_axis',(-1.79091352057933E-16,2.24573452299033E-16,
1.));
#18406=DIRECTION('ref_axis',(-0.222520933956305,-0.974927912181826,1.79091352057932E-16));
#18407=DIRECTION('center_axis',(-1.79091352057933E-16,2.24573452299033E-16,
1.));
#18408=DIRECTION('ref_axis',(-0.222520933956305,-0.974927912181826,1.79091352057932E-16));
#18409=DIRECTION('center_axis',(-1.79091352057933E-16,2.24573452299033E-16,
1.));
#18410=DIRECTION('ref_axis',(-0.222520933956305,-0.974927912181826,1.79091352057932E-16));
#18411=DIRECTION('center_axis',(-0.974927912181826,0.222520933956305,-2.24573452299033E-16));
#18412=DIRECTION('ref_axis',(1.64444757441797E-16,-2.8874437615686E-16,
-1.));
#18413=DIRECTION('center_axis',(-0.974927912181826,0.222520933956305,-2.24573452299033E-16));
#18414=DIRECTION('ref_axis',(1.64444757441797E-16,-2.8874437615686E-16,
-1.));
#18415=DIRECTION('center_axis',(0.781831482468022,0.623489801858743,6.91638013500039E-17));
#18416=DIRECTION('ref_axis',(0.,0.,-1.));
#18417=DIRECTION('center_axis',(-0.781831482468022,-0.623489801858743,-6.91638013500039E-17));
#18418=DIRECTION('ref_axis',(5.40744373425973E-17,4.31229247995114E-17,
-1.));
#18419=DIRECTION('center_axis',(0.623489801858743,-0.781831482468022,-2.05955304247934E-16));
#18420=DIRECTION('ref_axis',(0.,-2.63426721571497E-16,1.));
#18421=DIRECTION('center_axis',(-0.781831482468022,-0.623489801858743,-6.91638013500039E-17));
#18422=DIRECTION('ref_axis',(5.40744373425973E-17,4.31229247995114E-17,
-1.));
#18423=DIRECTION('center_axis',(0.623489801858743,-0.781831482468022,-1.22464679914735E-16));
#18424=DIRECTION('ref_axis',(0.,0.,-1.));
#18425=DIRECTION('center_axis',(0.,0.,-1.));
#18426=DIRECTION('ref_axis',(1.,0.,0.));
#18427=DIRECTION('center_axis',(0.781831482468022,0.623489801858743,0.));
#18428=DIRECTION('ref_axis',(0.,0.,1.));
#18429=DIRECTION('center_axis',(-1.43620113371564E-16,6.91638013500039E-17,
1.));
#18430=DIRECTION('ref_axis',(0.623489801858743,-0.781831482468022,1.43620113371564E-16));
#18431=DIRECTION('center_axis',(-1.43620113371564E-16,6.91638013500039E-17,
1.));
#18432=DIRECTION('ref_axis',(0.623489801858743,-0.781831482468022,1.43620113371564E-16));
#18433=DIRECTION('center_axis',(-1.43620113371564E-16,6.91638013500039E-17,
1.));
#18434=DIRECTION('ref_axis',(0.623489801858743,-0.781831482468022,1.43620113371564E-16));
#18435=DIRECTION('center_axis',(0.,0.,-1.));
#18436=DIRECTION('ref_axis',(1.,0.,0.));
#18437=DIRECTION('center_axis',(0.,0.,-1.));
#18438=DIRECTION('ref_axis',(1.,0.,0.));
#18439=DIRECTION('center_axis',(-0.781831482468022,-0.623489801858743,-6.91638013500039E-17));
#18440=DIRECTION('ref_axis',(5.40744373425973E-17,4.31229247995114E-17,
-1.));
#18441=DIRECTION('center_axis',(-0.781831482468022,-0.623489801858743,-6.91638013500039E-17));
#18442=DIRECTION('ref_axis',(5.40744373425973E-17,4.31229247995114E-17,
-1.));
#18443=DIRECTION('center_axis',(1.,0.,-1.22464679914735E-16));
#18444=DIRECTION('ref_axis',(-6.12323399573677E-17,0.,-1.));
#18445=DIRECTION('center_axis',(1.43620113371566E-16,6.91638013500059E-17,
1.));
#18446=DIRECTION('ref_axis',(1.,-1.10509814492274E-33,-1.43620113371566E-16));
#18447=DIRECTION('center_axis',(1.43620113371566E-16,6.91638013500059E-17,
1.));
#18448=DIRECTION('ref_axis',(1.,-1.10509814492274E-33,-1.43620113371566E-16));
#18449=DIRECTION('center_axis',(1.43620113371566E-16,6.91638013500059E-17,
1.));
#18450=DIRECTION('ref_axis',(1.,-1.10509814492274E-33,-1.43620113371566E-16));
#18451=DIRECTION('center_axis',(0.,1.,0.));
#18452=DIRECTION('ref_axis',(6.12323399573677E-17,0.,1.));
#18453=DIRECTION('center_axis',(0.,0.,1.));
#18454=DIRECTION('ref_axis',(1.,0.,0.));
#18455=DIRECTION('center_axis',(0.,0.,1.));
#18456=DIRECTION('ref_axis',(1.,0.,0.));
#18457=DIRECTION('center_axis',(0.,0.,1.));
#18458=DIRECTION('ref_axis',(1.,0.,0.));
#18459=DIRECTION('center_axis',(0.,-1.,0.));
#18460=DIRECTION('ref_axis',(0.,0.,-1.));
#18461=DIRECTION('center_axis',(0.,-1.,0.));
#18462=DIRECTION('ref_axis',(0.,0.,-1.));
#18463=DIRECTION('center_axis',(0.,1.,0.));
#18464=DIRECTION('ref_axis',(0.,0.,-1.));
#18465=DIRECTION('center_axis',(0.,-1.,0.));
#18466=DIRECTION('ref_axis',(0.,0.,-1.));
#18467=DIRECTION('center_axis',(1.,0.,-1.22464679914735E-16));
#18468=DIRECTION('ref_axis',(1.22464679914735E-16,0.,1.));
#18469=DIRECTION('center_axis',(0.,-1.,0.));
#18470=DIRECTION('ref_axis',(0.,0.,-1.));
#18471=DIRECTION('center_axis',(0.,0.,-1.));
#18472=DIRECTION('ref_axis',(-1.,0.,0.));
#18473=DIRECTION('center_axis',(0.,0.,-1.));
#18474=DIRECTION('ref_axis',(1.,0.,0.));
#18475=DIRECTION('center_axis',(0.,0.,-1.));
#18476=DIRECTION('ref_axis',(1.,0.,0.));
#18477=DIRECTION('center_axis',(0.,0.,-1.));
#18478=DIRECTION('ref_axis',(-1.,0.,0.));
#18479=DIRECTION('center_axis',(0.,0.,1.));
#18480=DIRECTION('ref_axis',(1.,0.,0.));
#18481=DIRECTION('center_axis',(0.,0.,1.));
#18482=DIRECTION('ref_axis',(1.,0.,0.));
#18483=DIRECTION('center_axis',(0.,0.,1.));
#18484=DIRECTION('ref_axis',(1.,0.,0.));
#18485=DIRECTION('center_axis',(0.,0.,1.));
#18486=DIRECTION('ref_axis',(1.,0.,0.));
#18487=DIRECTION('center_axis',(0.,-1.,0.));
#18488=DIRECTION('ref_axis',(0.,0.,-1.));
#18489=DIRECTION('center_axis',(0.,1.,0.));
#18490=DIRECTION('ref_axis',(0.,0.,1.));
#18491=DIRECTION('center_axis',(0.,0.,1.));
#18492=DIRECTION('ref_axis',(1.,0.,0.));
#18493=DIRECTION('center_axis',(0.,0.,-1.));
#18494=DIRECTION('ref_axis',(1.,0.,0.));
#18495=DIRECTION('center_axis',(0.,0.,1.));
#18496=DIRECTION('ref_axis',(1.,0.,0.));
#18497=DIRECTION('center_axis',(0.,0.,1.));
#18498=DIRECTION('ref_axis',(1.,0.,0.));
#18499=DIRECTION('center_axis',(0.,0.,1.));
#18500=DIRECTION('ref_axis',(1.,0.,0.));
#18501=DIRECTION('center_axis',(0.,0.,-1.));
#18502=DIRECTION('ref_axis',(1.,0.,0.));
#18503=DIRECTION('center_axis',(0.,0.,-1.));
#18504=DIRECTION('ref_axis',(-1.,0.,0.));
#18505=DIRECTION('center_axis',(0.,0.,-1.));
#18506=DIRECTION('ref_axis',(-1.,0.,0.));
#18507=DIRECTION('center_axis',(0.781831482468022,0.623489801858743,6.91638013500039E-17));
#18508=DIRECTION('ref_axis',(-1.43620113371564E-16,6.91638013500039E-17,
1.));
#18509=DIRECTION('center_axis',(-0.781831482468022,-0.623489801858743,-6.91638013500039E-17));
#18510=DIRECTION('ref_axis',(1.43620113371564E-16,-6.91638013500039E-17,
-1.));
#18511=DIRECTION('center_axis',(-1.43620113371564E-16,6.91638013500039E-17,
1.));
#18512=DIRECTION('ref_axis',(0.623489801858743,-0.781831482468022,1.43620113371564E-16));
#18513=DIRECTION('center_axis',(-1.43620113371564E-16,6.91638013500039E-17,
1.));
#18514=DIRECTION('ref_axis',(0.623489801858743,-0.781831482468022,1.43620113371564E-16));
#18515=DIRECTION('center_axis',(1.43620113371564E-16,-6.91638013500039E-17,
-1.));
#18516=DIRECTION('ref_axis',(0.623489801858743,-0.781831482468022,1.43620113371564E-16));
#18517=DIRECTION('center_axis',(-1.43620113371564E-16,6.91638013500039E-17,
1.));
#18518=DIRECTION('ref_axis',(0.623489801858743,-0.781831482468022,1.43620113371564E-16));
#18519=DIRECTION('center_axis',(1.43620113371564E-16,-6.91638013500039E-17,
-1.));
#18520=DIRECTION('ref_axis',(0.623489801858743,-0.781831482468022,1.43620113371564E-16));
#18521=DIRECTION('center_axis',(-1.43620113371564E-16,6.91638013500039E-17,
1.));
#18522=DIRECTION('ref_axis',(0.623489801858743,-0.781831482468022,1.43620113371564E-16));
#18523=DIRECTION('center_axis',(1.43620113371564E-16,-6.91638013500039E-17,
-1.));
#18524=DIRECTION('ref_axis',(-0.623489801858743,0.781831482468022,-1.43620113371564E-16));
#18525=DIRECTION('center_axis',(1.43620113371564E-16,-6.91638013500039E-17,
-1.));
#18526=DIRECTION('ref_axis',(-0.623489801858743,0.781831482468022,-1.43620113371564E-16));
#18527=DIRECTION('center_axis',(1.79091352057933E-16,-2.24573452299033E-16,
-1.));
#18528=DIRECTION('ref_axis',(0.222520933956305,0.974927912181826,-1.79091352057932E-16));
#18529=DIRECTION('center_axis',(1.79091352057933E-16,-2.24573452299033E-16,
-1.));
#18530=DIRECTION('ref_axis',(-0.222520933956305,-0.974927912181826,1.79091352057932E-16));
#18531=DIRECTION('center_axis',(1.79091352057933E-16,-2.24573452299033E-16,
-1.));
#18532=DIRECTION('ref_axis',(-0.222520933956305,-0.974927912181826,1.79091352057932E-16));
#18533=DIRECTION('center_axis',(1.79091352057933E-16,-2.24573452299033E-16,
-1.));
#18534=DIRECTION('ref_axis',(0.222520933956305,0.974927912181826,-1.79091352057932E-16));
#18535=DIRECTION('center_axis',(-1.79091352057933E-16,2.24573452299033E-16,
1.));
#18536=DIRECTION('ref_axis',(-0.222520933956305,-0.974927912181826,1.79091352057932E-16));
#18537=DIRECTION('center_axis',(-1.79091352057933E-16,2.24573452299033E-16,
1.));
#18538=DIRECTION('ref_axis',(-0.222520933956305,-0.974927912181826,1.79091352057932E-16));
#18539=DIRECTION('center_axis',(-1.79091352057933E-16,2.24573452299033E-16,
1.));
#18540=DIRECTION('ref_axis',(-0.222520933956305,-0.974927912181826,1.79091352057932E-16));
#18541=DIRECTION('center_axis',(-1.79091352057933E-16,2.24573452299033E-16,
1.));
#18542=DIRECTION('ref_axis',(-0.222520933956305,-0.974927912181826,1.79091352057932E-16));
#18543=DIRECTION('center_axis',(0.974927912181826,-0.222520933956305,2.24573452299033E-16));
#18544=DIRECTION('ref_axis',(-1.79091352057933E-16,2.24573452299033E-16,
1.));
#18545=DIRECTION('center_axis',(-0.974927912181826,0.222520933956305,-2.24573452299033E-16));
#18546=DIRECTION('ref_axis',(1.79091352057933E-16,-2.24573452299033E-16,
-1.));
#18547=DIRECTION('center_axis',(-1.79091352057933E-16,2.24573452299033E-16,
1.));
#18548=DIRECTION('ref_axis',(-0.222520933956305,-0.974927912181826,1.79091352057932E-16));
#18549=DIRECTION('center_axis',(-1.79091352057933E-16,2.24573452299033E-16,
1.));
#18550=DIRECTION('ref_axis',(-0.222520933956305,-0.974927912181826,1.79091352057932E-16));
#18551=DIRECTION('center_axis',(1.79091352057933E-16,-2.24573452299033E-16,
-1.));
#18552=DIRECTION('ref_axis',(-0.222520933956305,-0.974927912181826,1.79091352057932E-16));
#18553=DIRECTION('center_axis',(-1.79091352057933E-16,2.24573452299033E-16,
1.));
#18554=DIRECTION('ref_axis',(-0.222520933956305,-0.974927912181826,1.79091352057932E-16));
#18555=DIRECTION('center_axis',(1.79091352057933E-16,-2.24573452299033E-16,
-1.));
#18556=DIRECTION('ref_axis',(-0.222520933956305,-0.974927912181826,1.79091352057932E-16));
#18557=DIRECTION('center_axis',(-1.79091352057933E-16,2.24573452299033E-16,
1.));
#18558=DIRECTION('ref_axis',(-0.222520933956305,-0.974927912181826,1.79091352057932E-16));
#18559=DIRECTION('center_axis',(1.79091352057933E-16,-2.24573452299033E-16,
-1.));
#18560=DIRECTION('ref_axis',(0.222520933956305,0.974927912181826,-1.79091352057932E-16));
#18561=DIRECTION('center_axis',(1.79091352057933E-16,-2.24573452299033E-16,
-1.));
#18562=DIRECTION('ref_axis',(0.222520933956305,0.974927912181826,-1.79091352057932E-16));
#18563=DIRECTION('center_axis',(7.97031498468617E-17,-3.49202315903319E-16,
-1.));
#18564=DIRECTION('ref_axis',(0.900968867902416,0.433883739117565,-7.97031498468616E-17));
#18565=DIRECTION('center_axis',(7.97031498468617E-17,-3.49202315903319E-16,
-1.));
#18566=DIRECTION('ref_axis',(-0.900968867902416,-0.433883739117565,7.97031498468616E-17));
#18567=DIRECTION('center_axis',(7.97031498468617E-17,-3.49202315903319E-16,
-1.));
#18568=DIRECTION('ref_axis',(-0.900968867902416,-0.433883739117565,7.97031498468616E-17));
#18569=DIRECTION('center_axis',(7.97031498468617E-17,-3.49202315903319E-16,
-1.));
#18570=DIRECTION('ref_axis',(0.900968867902416,0.433883739117565,-7.97031498468616E-17));
#18571=DIRECTION('center_axis',(-7.97031498468617E-17,3.49202315903319E-16,
1.));
#18572=DIRECTION('ref_axis',(-0.900968867902416,-0.433883739117565,7.97031498468616E-17));
#18573=DIRECTION('center_axis',(-7.97031498468617E-17,3.49202315903319E-16,
1.));
#18574=DIRECTION('ref_axis',(-0.900968867902416,-0.433883739117565,7.97031498468616E-17));
#18575=DIRECTION('center_axis',(-7.97031498468617E-17,3.49202315903319E-16,
1.));
#18576=DIRECTION('ref_axis',(-0.900968867902416,-0.433883739117565,7.97031498468616E-17));
#18577=DIRECTION('center_axis',(-7.97031498468617E-17,3.49202315903319E-16,
1.));
#18578=DIRECTION('ref_axis',(-0.900968867902416,-0.433883739117565,7.97031498468616E-17));
#18579=DIRECTION('center_axis',(0.433883739117565,-0.900968867902416,3.49202315903319E-16));
#18580=DIRECTION('ref_axis',(-7.97031498468617E-17,3.49202315903319E-16,
1.));
#18581=DIRECTION('center_axis',(-0.433883739117565,0.900968867902416,-3.49202315903319E-16));
#18582=DIRECTION('ref_axis',(7.97031498468617E-17,-3.49202315903319E-16,
-1.));
#18583=DIRECTION('center_axis',(-7.97031498468617E-17,3.49202315903319E-16,
1.));
#18584=DIRECTION('ref_axis',(-0.900968867902416,-0.433883739117565,7.97031498468616E-17));
#18585=DIRECTION('center_axis',(-7.97031498468617E-17,3.49202315903319E-16,
1.));
#18586=DIRECTION('ref_axis',(-0.900968867902416,-0.433883739117565,7.97031498468616E-17));
#18587=DIRECTION('center_axis',(7.97031498468617E-17,-3.49202315903319E-16,
-1.));
#18588=DIRECTION('ref_axis',(-0.900968867902416,-0.433883739117565,7.97031498468616E-17));
#18589=DIRECTION('center_axis',(-7.97031498468617E-17,3.49202315903319E-16,
1.));
#18590=DIRECTION('ref_axis',(-0.900968867902416,-0.433883739117565,7.97031498468616E-17));
#18591=DIRECTION('center_axis',(7.97031498468617E-17,-3.49202315903319E-16,
-1.));
#18592=DIRECTION('ref_axis',(-0.900968867902416,-0.433883739117565,7.97031498468616E-17));
#18593=DIRECTION('center_axis',(-7.97031498468617E-17,3.49202315903319E-16,
1.));
#18594=DIRECTION('ref_axis',(-0.900968867902416,-0.433883739117565,7.97031498468616E-17));
#18595=DIRECTION('center_axis',(7.97031498468617E-17,-3.49202315903319E-16,
-1.));
#18596=DIRECTION('ref_axis',(0.900968867902416,0.433883739117565,-7.97031498468616E-17));
#18597=DIRECTION('center_axis',(7.97031498468617E-17,-3.49202315903319E-16,
-1.));
#18598=DIRECTION('ref_axis',(0.900968867902416,0.433883739117565,-7.97031498468616E-17));
#18599=DIRECTION('center_axis',(-7.97031498468594E-17,-3.4920231590332E-16,
-1.));
#18600=DIRECTION('ref_axis',(0.900968867902422,-0.433883739117553,7.97031498468594E-17));
#18601=DIRECTION('center_axis',(-7.97031498468594E-17,-3.4920231590332E-16,
-1.));
#18602=DIRECTION('ref_axis',(-0.900968867902422,0.433883739117553,-7.97031498468594E-17));
#18603=DIRECTION('center_axis',(-7.97031498468594E-17,-3.4920231590332E-16,
-1.));
#18604=DIRECTION('ref_axis',(-0.900968867902422,0.433883739117553,-7.97031498468594E-17));
#18605=DIRECTION('center_axis',(-7.97031498468594E-17,-3.4920231590332E-16,
-1.));
#18606=DIRECTION('ref_axis',(0.900968867902422,-0.433883739117553,7.97031498468594E-17));
#18607=DIRECTION('center_axis',(7.97031498468594E-17,3.4920231590332E-16,
1.));
#18608=DIRECTION('ref_axis',(-0.900968867902422,0.433883739117553,-7.97031498468594E-17));
#18609=DIRECTION('center_axis',(7.97031498468594E-17,3.4920231590332E-16,
1.));
#18610=DIRECTION('ref_axis',(-0.900968867902422,0.433883739117553,-7.97031498468594E-17));
#18611=DIRECTION('center_axis',(7.97031498468594E-17,3.4920231590332E-16,
1.));
#18612=DIRECTION('ref_axis',(-0.900968867902422,0.433883739117553,-7.97031498468594E-17));
#18613=DIRECTION('center_axis',(7.97031498468594E-17,3.4920231590332E-16,
1.));
#18614=DIRECTION('ref_axis',(-0.900968867902422,0.433883739117553,-7.97031498468594E-17));
#18615=DIRECTION('center_axis',(-0.433883739117553,-0.900968867902422,3.4920231590332E-16));
#18616=DIRECTION('ref_axis',(7.97031498468594E-17,3.4920231590332E-16,1.));
#18617=DIRECTION('center_axis',(0.433883739117553,0.900968867902422,-3.4920231590332E-16));
#18618=DIRECTION('ref_axis',(-7.97031498468594E-17,-3.4920231590332E-16,
-1.));
#18619=DIRECTION('center_axis',(7.97031498468594E-17,3.4920231590332E-16,
1.));
#18620=DIRECTION('ref_axis',(-0.900968867902422,0.433883739117553,-7.97031498468594E-17));
#18621=DIRECTION('center_axis',(7.97031498468594E-17,3.4920231590332E-16,
1.));
#18622=DIRECTION('ref_axis',(-0.900968867902422,0.433883739117553,-7.97031498468594E-17));
#18623=DIRECTION('center_axis',(-7.97031498468594E-17,-3.4920231590332E-16,
-1.));
#18624=DIRECTION('ref_axis',(-0.900968867902422,0.433883739117553,-7.97031498468594E-17));
#18625=DIRECTION('center_axis',(7.97031498468594E-17,3.4920231590332E-16,
1.));
#18626=DIRECTION('ref_axis',(-0.900968867902422,0.433883739117553,-7.97031498468594E-17));
#18627=DIRECTION('center_axis',(-7.97031498468594E-17,-3.4920231590332E-16,
-1.));
#18628=DIRECTION('ref_axis',(-0.900968867902422,0.433883739117553,-7.97031498468594E-17));
#18629=DIRECTION('center_axis',(7.97031498468594E-17,3.4920231590332E-16,
1.));
#18630=DIRECTION('ref_axis',(-0.900968867902422,0.433883739117553,-7.97031498468594E-17));
#18631=DIRECTION('center_axis',(-7.97031498468594E-17,-3.4920231590332E-16,
-1.));
#18632=DIRECTION('ref_axis',(0.900968867902422,-0.433883739117553,7.97031498468594E-17));
#18633=DIRECTION('center_axis',(-7.97031498468594E-17,-3.4920231590332E-16,
-1.));
#18634=DIRECTION('ref_axis',(0.900968867902422,-0.433883739117553,7.97031498468594E-17));
#18635=DIRECTION('center_axis',(-1.79091352057932E-16,-2.24573452299036E-16,
-1.));
#18636=DIRECTION('ref_axis',(0.222520933956318,-0.974927912181823,1.79091352057933E-16));
#18637=DIRECTION('center_axis',(-1.79091352057932E-16,-2.24573452299036E-16,
-1.));
#18638=DIRECTION('ref_axis',(-0.222520933956318,0.974927912181823,-1.79091352057933E-16));
#18639=DIRECTION('center_axis',(-1.79091352057932E-16,-2.24573452299036E-16,
-1.));
#18640=DIRECTION('ref_axis',(-0.222520933956318,0.974927912181823,-1.79091352057933E-16));
#18641=DIRECTION('center_axis',(-1.79091352057932E-16,-2.24573452299036E-16,
-1.));
#18642=DIRECTION('ref_axis',(0.222520933956318,-0.974927912181823,1.79091352057933E-16));
#18643=DIRECTION('center_axis',(1.79091352057932E-16,2.24573452299036E-16,
1.));
#18644=DIRECTION('ref_axis',(-0.222520933956318,0.974927912181823,-1.79091352057933E-16));
#18645=DIRECTION('center_axis',(1.79091352057932E-16,2.24573452299036E-16,
1.));
#18646=DIRECTION('ref_axis',(-0.222520933956318,0.974927912181823,-1.79091352057933E-16));
#18647=DIRECTION('center_axis',(1.79091352057932E-16,2.24573452299036E-16,
1.));
#18648=DIRECTION('ref_axis',(-0.222520933956318,0.974927912181823,-1.79091352057933E-16));
#18649=DIRECTION('center_axis',(1.79091352057932E-16,2.24573452299036E-16,
1.));
#18650=DIRECTION('ref_axis',(-0.222520933956318,0.974927912181823,-1.79091352057933E-16));
#18651=DIRECTION('center_axis',(-0.974927912181823,-0.222520933956318,2.24573452299036E-16));
#18652=DIRECTION('ref_axis',(1.79091352057932E-16,2.24573452299036E-16,
1.));
#18653=DIRECTION('center_axis',(0.974927912181823,0.222520933956318,-2.24573452299036E-16));
#18654=DIRECTION('ref_axis',(-1.79091352057932E-16,-2.24573452299036E-16,
-1.));
#18655=DIRECTION('center_axis',(1.79091352057932E-16,2.24573452299036E-16,
1.));
#18656=DIRECTION('ref_axis',(-0.222520933956318,0.974927912181823,-1.79091352057933E-16));
#18657=DIRECTION('center_axis',(1.79091352057932E-16,2.24573452299036E-16,
1.));
#18658=DIRECTION('ref_axis',(-0.222520933956318,0.974927912181823,-1.79091352057933E-16));
#18659=DIRECTION('center_axis',(-1.79091352057932E-16,-2.24573452299036E-16,
-1.));
#18660=DIRECTION('ref_axis',(-0.222520933956318,0.974927912181823,-1.79091352057933E-16));
#18661=DIRECTION('center_axis',(1.79091352057932E-16,2.24573452299036E-16,
1.));
#18662=DIRECTION('ref_axis',(-0.222520933956318,0.974927912181823,-1.79091352057933E-16));
#18663=DIRECTION('center_axis',(-1.79091352057932E-16,-2.24573452299036E-16,
-1.));
#18664=DIRECTION('ref_axis',(-0.222520933956318,0.974927912181823,-1.79091352057933E-16));
#18665=DIRECTION('center_axis',(1.79091352057932E-16,2.24573452299036E-16,
1.));
#18666=DIRECTION('ref_axis',(-0.222520933956318,0.974927912181823,-1.79091352057933E-16));
#18667=DIRECTION('center_axis',(-1.79091352057932E-16,-2.24573452299036E-16,
-1.));
#18668=DIRECTION('ref_axis',(0.222520933956318,-0.974927912181823,1.79091352057933E-16));
#18669=DIRECTION('center_axis',(-1.79091352057932E-16,-2.24573452299036E-16,
-1.));
#18670=DIRECTION('ref_axis',(0.222520933956318,-0.974927912181823,1.79091352057933E-16));
#18671=DIRECTION('center_axis',(-1.43620113371566E-16,-6.91638013500059E-17,
-1.));
#18672=DIRECTION('ref_axis',(-0.623489801858732,-0.781831482468031,1.43620113371566E-16));
#18673=DIRECTION('center_axis',(-1.43620113371566E-16,-6.91638013500059E-17,
-1.));
#18674=DIRECTION('ref_axis',(0.623489801858732,0.781831482468031,-1.43620113371566E-16));
#18675=DIRECTION('center_axis',(-1.43620113371566E-16,-6.91638013500059E-17,
-1.));
#18676=DIRECTION('ref_axis',(0.623489801858732,0.781831482468031,-1.43620113371566E-16));
#18677=DIRECTION('center_axis',(-1.43620113371566E-16,-6.91638013500059E-17,
-1.));
#18678=DIRECTION('ref_axis',(-0.623489801858732,-0.781831482468031,1.43620113371566E-16));
#18679=DIRECTION('center_axis',(1.43620113371566E-16,6.91638013500059E-17,
1.));
#18680=DIRECTION('ref_axis',(0.623489801858732,0.781831482468031,-1.43620113371566E-16));
#18681=DIRECTION('center_axis',(1.43620113371566E-16,6.91638013500059E-17,
1.));
#18682=DIRECTION('ref_axis',(0.623489801858732,0.781831482468031,-1.43620113371566E-16));
#18683=DIRECTION('center_axis',(1.43620113371566E-16,6.91638013500059E-17,
1.));
#18684=DIRECTION('ref_axis',(0.623489801858732,0.781831482468031,-1.43620113371566E-16));
#18685=DIRECTION('center_axis',(1.43620113371566E-16,6.91638013500059E-17,
1.));
#18686=DIRECTION('ref_axis',(0.623489801858732,0.781831482468031,-1.43620113371566E-16));
#18687=DIRECTION('center_axis',(-0.781831482468031,0.623489801858732,6.91638013500059E-17));
#18688=DIRECTION('ref_axis',(1.43620113371566E-16,6.91638013500061E-17,
1.));
#18689=DIRECTION('center_axis',(0.781831482468031,-0.623489801858732,-6.91638013500059E-17));
#18690=DIRECTION('ref_axis',(-1.43620113371566E-16,-6.91638013500061E-17,
-1.));
#18691=DIRECTION('center_axis',(1.43620113371566E-16,6.91638013500059E-17,
1.));
#18692=DIRECTION('ref_axis',(0.623489801858732,0.781831482468031,-1.43620113371566E-16));
#18693=DIRECTION('center_axis',(1.43620113371566E-16,6.91638013500059E-17,
1.));
#18694=DIRECTION('ref_axis',(0.623489801858732,0.781831482468031,-1.43620113371566E-16));
#18695=DIRECTION('center_axis',(-1.43620113371566E-16,-6.91638013500059E-17,
-1.));
#18696=DIRECTION('ref_axis',(0.623489801858732,0.781831482468031,-1.43620113371566E-16));
#18697=DIRECTION('center_axis',(1.43620113371566E-16,6.91638013500059E-17,
1.));
#18698=DIRECTION('ref_axis',(0.623489801858732,0.781831482468031,-1.43620113371566E-16));
#18699=DIRECTION('center_axis',(-1.43620113371566E-16,-6.91638013500059E-17,
-1.));
#18700=DIRECTION('ref_axis',(0.623489801858732,0.781831482468031,-1.43620113371566E-16));
#18701=DIRECTION('center_axis',(1.43620113371566E-16,6.91638013500059E-17,
1.));
#18702=DIRECTION('ref_axis',(0.623489801858732,0.781831482468031,-1.43620113371566E-16));
#18703=DIRECTION('center_axis',(-1.43620113371566E-16,-6.91638013500059E-17,
-1.));
#18704=DIRECTION('ref_axis',(-0.623489801858732,-0.781831482468031,1.43620113371566E-16));
#18705=DIRECTION('center_axis',(-1.43620113371566E-16,-6.91638013500059E-17,
-1.));
#18706=DIRECTION('ref_axis',(-0.623489801858732,-0.781831482468031,1.43620113371566E-16));
#18707=DIRECTION('center_axis',(0.,0.,1.));
#18708=DIRECTION('ref_axis',(1.,0.,0.));
#18709=DIRECTION('center_axis',(0.,0.,1.));
#18710=DIRECTION('ref_axis',(1.,0.,0.));
#18711=DIRECTION('center_axis',(0.,0.,-1.));
#18712=DIRECTION('ref_axis',(1.,0.,0.));
#18713=DIRECTION('center_axis',(0.,0.,1.));
#18714=DIRECTION('ref_axis',(1.,0.,0.));
#18715=DIRECTION('center_axis',(0.,0.,-1.));
#18716=DIRECTION('ref_axis',(1.,0.,0.));
#18717=DIRECTION('center_axis',(0.,0.,1.));
#18718=DIRECTION('ref_axis',(1.,0.,0.));
#18719=DIRECTION('center_axis',(0.,0.,-1.));
#18720=DIRECTION('ref_axis',(-1.,0.,0.));
#18721=DIRECTION('center_axis',(0.,0.,-1.));
#18722=DIRECTION('ref_axis',(-1.,0.,0.));
#42263=CARTESIAN_POINT('',(0.,0.,0.));
#42264=CARTESIAN_POINT('Origin',(0.,1.73472347597681E-15,6.67403582113016E-15));
#42265=CARTESIAN_POINT('',(1.52656933693714E-15,12.4653846153846,-3.0875));
#42266=CARTESIAN_POINT('Origin',(0.,6.26866080313552E-16,-3.0875));
#42267=CARTESIAN_POINT('',(-1.52656933693714E-15,12.4653846153846,3.0875));
#42268=CARTESIAN_POINT('Origin',(1.74512168878498E-15,14.25,4.05635328795269E-15));
#42269=CARTESIAN_POINT('Origin',(0.,1.76119517802379E-15,3.0875));
#42270=CARTESIAN_POINT('Origin',(0.,1.56496838953657E-16,-5.64807088834312));
#42271=CARTESIAN_POINT('',(9.67029207191279E-16,7.64278544417155,-5.99278544417156));
#42272=CARTESIAN_POINT('',(9.35971273077467E-16,-7.64278544417155,-5.99278544417156));
#42273=CARTESIAN_POINT('Origin',(0.,9.31738023414375E-17,-5.99278544417156));
#42274=CARTESIAN_POINT('',(9.18485099360515E-16,-7.5,-5.64807088834312));
#42275=CARTESIAN_POINT('Origin',(9.78186630818948E-16,-7.9875,-5.64807088834312));
#42276=CARTESIAN_POINT('',(9.18485099360515E-16,7.5,-5.64807088834312));
#42277=CARTESIAN_POINT('Origin',(0.,1.56496838953657E-16,-5.64807088834312));
#42278=CARTESIAN_POINT('Origin',(0.,1.56496838953657E-16,-5.64807088834312));
#42279=CARTESIAN_POINT('Origin',(0.,9.31738023414375E-17,-5.99278544417156));
#42280=CARTESIAN_POINT('Origin',(0.,2.23156441938368E-15,5.64807088834312));
#42281=CARTESIAN_POINT('',(9.18485099360515E-16,7.5,5.64807088834312));
#42282=CARTESIAN_POINT('',(9.18485099360515E-16,-7.5,5.64807088834312));
#42283=CARTESIAN_POINT('Origin',(0.,2.23156441938368E-15,5.64807088834312));
#42284=CARTESIAN_POINT('',(-9.35971273077467E-16,-7.64278544417155,5.99278544417156));
#42285=CARTESIAN_POINT('Origin',(9.78186630818948E-16,-7.9875,5.64807088834312));
#42286=CARTESIAN_POINT('Origin',(0.,2.2948874559959E-15,5.99278544417156));
#42287=CARTESIAN_POINT('Origin',(0.,2.23156441938368E-15,5.64807088834312));
#42288=CARTESIAN_POINT('Origin',(0.,-9.99635681210842E-31,-6.5));
#42289=CARTESIAN_POINT('',(-9.98087141305092E-16,8.14999999999999,-6.50000000000001));
#42290=CARTESIAN_POINT('',(9.98087141305092E-16,8.14999999999999,-6.5));
#42291=CARTESIAN_POINT('Origin',(0.,-9.99635681210842E-31,-6.5));
#42292=CARTESIAN_POINT('Origin',(0.,0.,-6.5));
#42293=CARTESIAN_POINT('',(-9.18485099360515E-16,7.5,-6.5));
#42294=CARTESIAN_POINT('Origin',(0.,2.26865819542047E-15,5.85));
#42295=CARTESIAN_POINT('',(-9.98087141305091E-16,-8.14999999999998,6.50000000000001));
#42296=CARTESIAN_POINT('',(9.18485099360515E-16,-7.5,5.85));
#42297=CARTESIAN_POINT('Origin',(0.,2.38806125833734E-15,6.50000000000001));
#42298=CARTESIAN_POINT('Origin',(0.,0.,-6.5));
#42299=CARTESIAN_POINT('',(-1.52656933693714E-15,12.4653846153846,6.50000000000001));
#42300=CARTESIAN_POINT('Origin',(0.,2.38806125833734E-15,6.50000000000001));
#42301=CARTESIAN_POINT('',(-1.52656933693714E-15,12.4653846153846,-6.5));
#42302=CARTESIAN_POINT('Origin',(0.,0.,-6.5));
#42303=CARTESIAN_POINT('',(-1.52656933693714E-15,12.4653846153846,-6.50000000000001));
#42304=CARTESIAN_POINT('',(-1.52656933693714E-15,12.4653846153846,-6.5));
#42305=CARTESIAN_POINT('Origin',(0.,-1.17267830746035E-30,-6.50000000000001));
#42306=CARTESIAN_POINT('Origin',(0.,8.14999999999999,-6.50000000000001));
#42307=CARTESIAN_POINT('Origin',(0.,8.14999999999999,6.50000000000001));
#42308=CARTESIAN_POINT('Origin',(0.,14.25,4.07195060716495E-15));
#42309=CARTESIAN_POINT('',(-3.56616156686793,14.25,4.07195060716495E-15));
#42310=CARTESIAN_POINT('',(3.56616156686793,14.25,4.07195060716495E-15));
#42311=CARTESIAN_POINT('Origin',(0.,14.25,4.07195060716495E-15));
#42312=CARTESIAN_POINT('Origin',(11.1410986251694,8.88472967648693,5.05753477640253E-15));
#42313=CARTESIAN_POINT('',(8.91763325644669,11.6728670610318,4.54536224786764E-15));
#42314=CARTESIAN_POINT('',(13.3645639938921,6.09659229194206,5.56970730493742E-15));
#42315=CARTESIAN_POINT('Origin',(11.1410986251694,8.88472967648693,5.05753477640253E-15));
#42316=CARTESIAN_POINT('Origin',(13.892722748591,-3.17092330887753,7.27212230242621E-15));
#42317=CARTESIAN_POINT('',(14.6862683510896,0.305827142012077,6.6334536057588E-15));
#42318=CARTESIAN_POINT('',(13.0991771460924,-6.64767375976714,7.91079099909362E-15));
#42319=CARTESIAN_POINT('Origin',(13.892722748591,-3.17092330887753,7.27212230242621E-15));
#42320=CARTESIAN_POINT('Origin',(6.18284328242512,-12.8388063676095,9.04808360878726E-15));
#42321=CARTESIAN_POINT('',(9.39584383208325,-11.2915068526795,8.76384929904507E-15));
#42322=CARTESIAN_POINT('',(2.96984273276699,-14.3861058825395,9.33231791852945E-15));
#42323=CARTESIAN_POINT('Origin',(6.18284328242512,-12.8388063676095,9.04808360878726E-15));
#42324=CARTESIAN_POINT('Origin',(-6.1828432824253,-12.8388063676094,9.04808360878725E-15));
#42325=CARTESIAN_POINT('',(-2.9698427327672,-14.3861058825394,9.33231791852944E-15));
#42326=CARTESIAN_POINT('',(-9.39584383208341,-11.2915068526794,8.76384929904506E-15));
#42327=CARTESIAN_POINT('Origin',(-6.1828432824253,-12.8388063676094,9.04808360878725E-15));
#42328=CARTESIAN_POINT('Origin',(-13.892722748591,-3.17092330887735,7.27212230242617E-15));
#42329=CARTESIAN_POINT('',(-13.0991771460925,-6.64767375976697,7.91079099909359E-15));
#42330=CARTESIAN_POINT('',(-14.6862683510895,0.30582714201227,6.63345360575876E-15));
#42331=CARTESIAN_POINT('Origin',(-13.892722748591,-3.17092330887735,7.27212230242617E-15));
#42332=CARTESIAN_POINT('Origin',(-11.1410986251693,8.88472967648709,5.0575347764025E-15));
#42333=CARTESIAN_POINT('',(-13.3645639938921,6.09659229194225,5.56970730493739E-15));
#42334=CARTESIAN_POINT('',(-8.91763325644655,11.6728670610319,4.54536224786761E-15));
#42335=CARTESIAN_POINT('Origin',(-11.1410986251693,8.88472967648709,5.0575347764025E-15));
#42336=CARTESIAN_POINT('Origin',(0.,1.07462756625201E-17,-6.44149999999999));
#42337=CARTESIAN_POINT('',(-1.99949495950787E-15,-16.3271153846154,-6.49999999999999));
#42338=CARTESIAN_POINT('Origin',(0.,2.01169401222323E-30,-6.49999999999999));
#42339=CARTESIAN_POINT('',(1.99233077573286E-15,-16.2686153846154,-6.44149999999999));
#42340=CARTESIAN_POINT('Origin',(1.99949495950788E-15,-16.3271153846154,
-6.44149999999999));
#42341=CARTESIAN_POINT('',(1.99233077573286E-15,16.2686153846154,-6.44149999999999));
#42342=CARTESIAN_POINT('Origin',(0.,1.07462756625199E-17,-6.44149999999999));
#42343=CARTESIAN_POINT('Origin',(0.,1.07462756625199E-17,-6.44149999999999));
#42344=CARTESIAN_POINT('Origin',(0.,1.30149338579385E-16,-5.7915));
#42345=CARTESIAN_POINT('',(-1.96367404063281E-15,16.0346153846154,-5.7915));
#42346=CARTESIAN_POINT('Origin',(0.,1.30149338579385E-16,-5.7915));
#42347=CARTESIAN_POINT('',(-1.97083822440782E-15,16.0931153846154,-5.85));
#42348=CARTESIAN_POINT('Origin',(1.97083822440783E-15,16.0931153846154,
-5.7915));
#42349=CARTESIAN_POINT('Origin',(0.,1.19403062916867E-16,-5.85));
#42350=CARTESIAN_POINT('Origin',(0.,2.37731498267482E-15,6.44150000000001));
#42351=CARTESIAN_POINT('',(-1.99949495950787E-15,16.3271153846154,6.5));
#42352=CARTESIAN_POINT('Origin',(0.,2.38806125833734E-15,6.50000000000001));
#42353=CARTESIAN_POINT('',(-1.99233077573286E-15,16.2686153846154,6.4415));
#42354=CARTESIAN_POINT('Origin',(1.99949495950788E-15,16.3271153846154,
6.44150000000001));
#42355=CARTESIAN_POINT('Origin',(0.,2.37731498267482E-15,6.44150000000001));
#42356=CARTESIAN_POINT('Origin',(0.,2.25791191975795E-15,5.7915));
#42357=CARTESIAN_POINT('',(1.96367404063281E-15,16.0346153846154,5.7915));
#42358=CARTESIAN_POINT('',(1.96367404063282E-15,-16.0346153846154,5.7915));
#42359=CARTESIAN_POINT('Origin',(0.,2.25791191975795E-15,5.7915));
#42360=CARTESIAN_POINT('',(-1.97083822440782E-15,-16.0931153846154,5.85000000000001));
#42361=CARTESIAN_POINT('Origin',(1.97083822440783E-15,-16.0931153846154,
5.7915));
#42362=CARTESIAN_POINT('Origin',(0.,2.26865819542047E-15,5.85));
#42363=CARTESIAN_POINT('Origin',(0.,2.25791191975795E-15,5.7915));
#42364=CARTESIAN_POINT('Origin',(0.,0.,-6.5));
#42365=CARTESIAN_POINT('',(-2.16636878649169E-15,17.6897435897436,-6.084));
#42366=CARTESIAN_POINT('Origin',(0.,7.6417960266795E-17,-6.084));
#42367=CARTESIAN_POINT('',(-2.16636878649169E-15,17.6897435897436,-5.85));
#42368=CARTESIAN_POINT('',(-2.16636878649169E-15,17.6897435897436,-6.5));
#42369=CARTESIAN_POINT('Origin',(0.,1.19403062916867E-16,-5.85));
#42370=CARTESIAN_POINT('Origin',(0.,0.,-6.5));
#42371=CARTESIAN_POINT('',(-1.99233077573286E-15,16.2686153846154,-6.084));
#42372=CARTESIAN_POINT('',(-1.99233077573286E-15,16.2686153846154,-6.5));
#42373=CARTESIAN_POINT('Origin',(0.,7.6417960266795E-17,-6.084));
#42374=CARTESIAN_POINT('Origin',(0.,0.,-6.5));
#42375=CARTESIAN_POINT('',(-1.96367404063281E-15,16.0346153846154,3.0875));
#42376=CARTESIAN_POINT('Origin',(0.,1.76119517802379E-15,3.08750000000001));
#42377=CARTESIAN_POINT('',(-1.96367404063282E-15,16.0346153846154,-6.5));
#42378=CARTESIAN_POINT('Origin',(0.,1.73472347597681E-15,6.67403582113016E-15));
#42379=CARTESIAN_POINT('',(-1.96367404063281E-15,16.0346153846154,-3.0875));
#42380=CARTESIAN_POINT('Origin',(1.74512168878498E-15,14.25,4.05635328795269E-15));
#42381=CARTESIAN_POINT('Origin',(0.,6.26866080313552E-16,-3.08749999999999));
#42382=CARTESIAN_POINT('Origin',(0.,0.,-6.5));
#42383=CARTESIAN_POINT('',(-1.96367404063282E-15,16.0346153846154,-6.5));
#42384=CARTESIAN_POINT('Origin',(0.,0.,-6.5));
#42385=CARTESIAN_POINT('',(-1.99233077573286E-15,16.2686153846154,6.084));
#42386=CARTESIAN_POINT('Origin',(0.,2.31164329807054E-15,6.084));
#42387=CARTESIAN_POINT('',(-1.99233077573286E-15,16.2686153846154,-6.5));
#42388=CARTESIAN_POINT('Origin',(0.,0.,-6.5));
#42389=CARTESIAN_POINT('',(-2.16636878649169E-15,17.6897435897436,5.85));
#42390=CARTESIAN_POINT('Origin',(0.,2.26865819542047E-15,5.85));
#42391=CARTESIAN_POINT('',(-2.16636878649169E-15,17.6897435897436,6.084));
#42392=CARTESIAN_POINT('',(-2.16636878649169E-15,17.6897435897436,-6.5));
#42393=CARTESIAN_POINT('Origin',(0.,2.31164329807054E-15,6.084));
#42394=CARTESIAN_POINT('Origin',(0.,2.38806125833734E-15,6.50000000000001));
#42395=CARTESIAN_POINT('',(-2.57175827820944E-15,21.,5.85));
#42396=CARTESIAN_POINT('Origin',(0.,2.26865819542047E-15,5.85000000000001));
#42397=CARTESIAN_POINT('',(-2.49215623626487E-15,20.35,6.5));
#42398=CARTESIAN_POINT('',(2.49215623626486E-15,20.35,6.50000000000001));
#42399=CARTESIAN_POINT('Origin',(0.,2.38806125833734E-15,6.50000000000001));
#42400=CARTESIAN_POINT('Origin',(0.,1.19403062916869E-16,-5.84999999999999));
#42401=CARTESIAN_POINT('',(2.57175827820944E-15,21.,-5.84999999999999));
#42402=CARTESIAN_POINT('',(2.57175827820944E-15,-21.,-5.84999999999999));
#42403=CARTESIAN_POINT('Origin',(0.,1.19403062916869E-16,-5.84999999999999));
#42404=CARTESIAN_POINT('Origin',(0.,1.19403062916869E-16,-5.84999999999999));
#42405=CARTESIAN_POINT('',(-2.49215623626487E-15,-20.35,-6.49999999999999));
#42406=CARTESIAN_POINT('',(2.57175827820944E-15,-21.,-5.84999999999999));
#42407=CARTESIAN_POINT('Origin',(0.,1.96135664184276E-30,-6.49999999999999));
#42408=CARTESIAN_POINT('Origin',(0.,0.,-6.5));
#42409=CARTESIAN_POINT('',(-2.57175827820944E-15,21.,-6.5));
#42410=CARTESIAN_POINT('Origin',(0.,20.35,-6.49999999999999));
#42411=CARTESIAN_POINT('Origin',(0.,20.35,6.5));
#42412=CARTESIAN_POINT('Origin',(0.,16.0346153846154,5.85));
#42413=CARTESIAN_POINT('Origin',(0.,16.2686153846154,6.084));
#42414=CARTESIAN_POINT('Origin',(0.,16.2686153846154,-6.084));
#42415=CARTESIAN_POINT('Origin',(0.,16.0346153846154,-5.85));
#42416=CARTESIAN_POINT('Origin',(-11.1410986251694,8.88472967648693,9.85584169237584E-16));
#42417=CARTESIAN_POINT('',(-11.838732871064,9.44107442276088,3.96060240207311));
#42418=CARTESIAN_POINT('Origin',(-11.838732871064,9.44107442276088,1.04729956121144E-15));
#42419=CARTESIAN_POINT('',(-10.4434643792749,8.32838493021299,3.96060240207311));
#42420=CARTESIAN_POINT('Origin',(-11.1410986251694,8.88472967648693,2.5198520116158));
#42421=CARTESIAN_POINT('Origin',(-10.4434643792749,8.32838493021299,9.23868777263733E-16));
#42422=CARTESIAN_POINT('',(-13.176267261227,5.42664547033602,-1.08333333333333));
#42423=CARTESIAN_POINT('',(-13.9269936544441,5.94376395877182,-1.08333333333333));
#42424=CARTESIAN_POINT('Ctrl Pts',(-13.176267261227,5.42664547033603,-1.08333333333333));
#42425=CARTESIAN_POINT('Ctrl Pts',(-13.3544742809805,5.48608062863209,-1.08333333333333));
#42426=CARTESIAN_POINT('Ctrl Pts',(-13.5395781511317,5.58798093945111,-1.08333333333333));
#42427=CARTESIAN_POINT('Ctrl Pts',(-13.7657237213497,5.76832601371359,-1.08333333333333));
#42428=CARTESIAN_POINT('Ctrl Pts',(-13.851789663848,5.85187873682469,-1.08333333333333));
#42429=CARTESIAN_POINT('Ctrl Pts',(-13.9269936544446,5.9437639587714,-1.08333333333333));
#42430=CARTESIAN_POINT('',(-13.9269936544455,5.94376395877242,1.08333333333333));
#42431=CARTESIAN_POINT('Ctrl Pts',(-13.9269936544444,5.94376395877114,1.08333333333355));
#42432=CARTESIAN_POINT('Ctrl Pts',(-13.9416885168396,5.90933203032471,0.95688863210348));
#42433=CARTESIAN_POINT('Ctrl Pts',(-13.9536527109306,5.88095561854246,0.828820583351296));
#42434=CARTESIAN_POINT('Ctrl Pts',(-13.9629765258054,5.85873440158612,0.699646919261824));
#42435=CARTESIAN_POINT('Ctrl Pts',(-13.9722513158078,5.83663002439321,0.571152453813156));
#42436=CARTESIAN_POINT('Ctrl Pts',(-13.9789135007646,5.82061622745832,0.441563969171476));
#42437=CARTESIAN_POINT('Ctrl Pts',(-13.9830050237945,5.81077040959789,0.311391073637591));
#42438=CARTESIAN_POINT('Ctrl Pts',(-13.9870637119681,5.80100360534983,0.182262827807202));
#42439=CARTESIAN_POINT('Ctrl Pts',(-13.9885928700523,5.79730615639837,0.0525595133518154));
#42440=CARTESIAN_POINT('Ctrl Pts',(-13.9875862925321,5.79973378332902,-0.0772214321948836));
#42441=CARTESIAN_POINT('Ctrl Pts',(-13.9868997670034,5.80138952054624,-0.16573715053464));
#42442=CARTESIAN_POINT('Ctrl Pts',(-13.9850326975558,5.80589410253377,-0.25428898113034));
#42443=CARTESIAN_POINT('Ctrl Pts',(-13.9819702480149,5.81325986277477,-0.342719102199523));
#42444=CARTESIAN_POINT('Ctrl Pts',(-13.9773533484511,5.82436436418404,-0.476034927301742));
#42445=CARTESIAN_POINT('Ctrl Pts',(-13.9700489046451,5.84190742581559,-0.608312350205735));
#42446=CARTESIAN_POINT('Ctrl Pts',(-13.9600480872369,5.86570879353503,-0.739057191237609));
#42447=CARTESIAN_POINT('Ctrl Pts',(-13.9511688384278,5.8868408927778,-0.855139299994326));
#42448=CARTESIAN_POINT('Ctrl Pts',(-13.9401632237806,5.9129059856334,-0.970013302477931));
#42449=CARTESIAN_POINT('Ctrl Pts',(-13.9269936544444,5.94376395877114,-1.08333333333355));
#42450=CARTESIAN_POINT('',(-13.176267261227,5.42664547033602,1.08333333333333));
#42451=CARTESIAN_POINT('Ctrl Pts',(-13.176267261227,5.42664547033603,1.08333333333333));
#42452=CARTESIAN_POINT('Ctrl Pts',(-13.3544742809805,5.48608062863209,1.08333333333333));
#42453=CARTESIAN_POINT('Ctrl Pts',(-13.5395781511317,5.58798093945111,1.08333333333333));
#42454=CARTESIAN_POINT('Ctrl Pts',(-13.76572372135,5.76832601371385,1.08333333333333));
#42455=CARTESIAN_POINT('Ctrl Pts',(-13.8517896638487,5.85187873682532,1.08333333333333));
#42456=CARTESIAN_POINT('Ctrl Pts',(-13.9269936544455,5.94376395877245,1.08333333333333));
#42457=CARTESIAN_POINT('Ctrl Pts',(-13.176267261227,5.426645470336,-1.08333333333333));
#42458=CARTESIAN_POINT('Ctrl Pts',(-13.1893705593041,5.39482976422217,-0.949270311030458));
#42459=CARTESIAN_POINT('Ctrl Pts',(-13.1999097963793,5.36892368585873,-0.813521288367943));
#42460=CARTESIAN_POINT('Ctrl Pts',(-13.2079621630869,5.34904061477063,-0.676607052100963));
#42461=CARTESIAN_POINT('Ctrl Pts',(-13.2148460430323,5.33204279546006,-0.559560573777783));
#42462=CARTESIAN_POINT('Ctrl Pts',(-13.2199117356377,5.31944645364942,-0.441662516279014));
#42463=CARTESIAN_POINT('Ctrl Pts',(-13.2231796369648,5.31131059989529,-0.323238258334693));
#42464=CARTESIAN_POINT('Ctrl Pts',(-13.2269557156994,5.30190957419894,-0.186398348762648));
#42465=CARTESIAN_POINT('Ctrl Pts',(-13.2283213471704,5.29849241313602,-0.0492519096262365));
#42466=CARTESIAN_POINT('Ctrl Pts',(-13.2273014856384,5.30103720115478,0.0876758270660023));
#42467=CARTESIAN_POINT('Ctrl Pts',(-13.2262786675027,5.30358936657696,0.225000520654269));
#42468=CARTESIAN_POINT('Ctrl Pts',(-13.2228564747501,5.31213809759637,0.362105241912721));
#42469=CARTESIAN_POINT('Ctrl Pts',(-13.21701132539,5.32664168351063,0.498460177595569));
#42470=CARTESIAN_POINT('Ctrl Pts',(-13.2111409592134,5.34120783998416,0.635403368116636));
#42471=CARTESIAN_POINT('Ctrl Pts',(-13.2028266475275,5.36178038996277,0.771590289741212));
#42472=CARTESIAN_POINT('Ctrl Pts',(-13.1919958930595,5.38829698119001,0.90648424252654));
#42473=CARTESIAN_POINT('Ctrl Pts',(-13.1872415508606,5.39993688577963,0.965698216399817));
#42474=CARTESIAN_POINT('Ctrl Pts',(-13.1820016856382,5.4127218947045,1.02466304565395));
#42475=CARTESIAN_POINT('Ctrl Pts',(-13.176267261227,5.426645470336,1.08333333333333));
#42476=CARTESIAN_POINT('',(-8.89378902201695,12.2552029391753,-1.08333333333333));
#42477=CARTESIAN_POINT('',(-8.22258343557141,11.6383685130291,-1.08333333333333));
#42478=CARTESIAN_POINT('Ctrl Pts',(-8.89378902201693,12.2552029391753,-1.08333333333333));
#42479=CARTESIAN_POINT('Ctrl Pts',(-8.78747309219938,12.2023308550396,-1.08333333333333));
#42480=CARTESIAN_POINT('Ctrl Pts',(-8.68686373639314,12.1370149953911,-1.08333333333333));
#42481=CARTESIAN_POINT('Ctrl Pts',(-8.46071816617524,11.9566699211287,-1.08333333333333));
#42482=CARTESIAN_POINT('Ctrl Pts',(-8.32018322283281,11.7988819437994,-1.08333333333333));
#42483=CARTESIAN_POINT('Ctrl Pts',(-8.22258343557192,11.6383685130288,-1.08333333333333));
#42484=CARTESIAN_POINT('',(-8.22258343557665,11.6383685130365,1.08333333333333));
#42485=CARTESIAN_POINT('Ctrl Pts',(-8.22258343557191,11.6383685130287,1.08333333333318));
#42486=CARTESIAN_POINT('Ctrl Pts',(-8.19455490688727,11.6581708517696,0.949622058007629));
#42487=CARTESIAN_POINT('Ctrl Pts',(-8.17172113698899,11.6741565633286,0.814376693553349));
#42488=CARTESIAN_POINT('Ctrl Pts',(-8.15417398891324,11.6864000683928,0.678132403728345));
#42489=CARTESIAN_POINT('Ctrl Pts',(-8.13671023659264,11.698585384152,0.542535637671064));
#42490=CARTESIAN_POINT('Ctrl Pts',(-8.12448291951145,11.7070640382822,0.405949418799179));
#42491=CARTESIAN_POINT('Ctrl Pts',(-8.11755242812626,11.7118675955896,0.268901316712111));
#42492=CARTESIAN_POINT('Ctrl Pts',(-8.11302715126356,11.7150040870061,0.179415511018989));
#42493=CARTESIAN_POINT('Ctrl Pts',(-8.11075954642953,11.7165728598427,0.0897327832367744));
#42494=CARTESIAN_POINT('Ctrl Pts',(-8.11075954642953,11.7165728598427,9.99200722162641E-15));
#42495=CARTESIAN_POINT('Ctrl Pts',(-8.11075954642954,11.7165728598427,-0.137573936980354));
#42496=CARTESIAN_POINT('Ctrl Pts',(-8.11609005089583,11.7128881555246,-0.274951212619692));
#42497=CARTESIAN_POINT('Ctrl Pts',(-8.12669452775723,11.7055258768037,-0.4116124062147));
#42498=CARTESIAN_POINT('Ctrl Pts',(-8.13738105388554,11.6981066344457,-0.549330978772881));
#42499=CARTESIAN_POINT('Ctrl Pts',(-8.15342350530942,11.6869526399855,-0.686322345437031));
#42500=CARTESIAN_POINT('Ctrl Pts',(-8.17473347641523,11.6720277839618,-0.822054935347404));
#42501=CARTESIAN_POINT('Ctrl Pts',(-8.18849695174643,11.662388264195,-0.909720570537357));
#42502=CARTESIAN_POINT('Ctrl Pts',(-8.20445714658991,11.6511748546878,-0.996861109122827));
#42503=CARTESIAN_POINT('Ctrl Pts',(-8.22258343557191,11.6383685130287,-1.08333333333318));
#42504=CARTESIAN_POINT('',(-8.89378902201695,12.2552029391753,1.08333333333333));
#42505=CARTESIAN_POINT('Ctrl Pts',(-8.89378902201693,12.2552029391753,1.08333333333333));
#42506=CARTESIAN_POINT('Ctrl Pts',(-8.78747309219938,12.2023308550396,1.08333333333333));
#42507=CARTESIAN_POINT('Ctrl Pts',(-8.68686373639314,12.1370149953911,1.08333333333333));
#42508=CARTESIAN_POINT('Ctrl Pts',(-8.46071816617751,11.9566699211305,1.08333333333333));
#42509=CARTESIAN_POINT('Ctrl Pts',(-8.32018322283717,11.7988819438045,1.08333333333333));
#42510=CARTESIAN_POINT('Ctrl Pts',(-8.22258343557662,11.6383685130365,1.08333333333333));
#42511=CARTESIAN_POINT('Ctrl Pts',(-8.89378902201696,12.2552029391753,-1.08333333333333));
#42512=CARTESIAN_POINT('Ctrl Pts',(-8.86325700199161,12.2773604951023,-0.955915065626613));
#42513=CARTESIAN_POINT('Ctrl Pts',(-8.83806624000395,12.2954729083691,-0.8267015714506));
#42514=CARTESIAN_POINT('Ctrl Pts',(-8.81837639229442,12.3095783864577,-0.696211209492237));
#42515=CARTESIAN_POINT('Ctrl Pts',(-8.79899689851553,12.3234615321731,-0.567777653525536));
#42516=CARTESIAN_POINT('Ctrl Pts',(-8.7849462329058,12.3334631509294,-0.438107164856251));
#42517=CARTESIAN_POINT('Ctrl Pts',(-8.77634666705863,12.3395794672318,-0.307693975181527));
#42518=CARTESIAN_POINT('Ctrl Pts',(-8.76960830208466,12.3443720314467,-0.205506064179221));
#42519=CARTESIAN_POINT('Ctrl Pts',(-8.76621624622179,12.3467783236356,-0.102862147741002));
#42520=CARTESIAN_POINT('Ctrl Pts',(-8.76621624622179,12.3467783236356,2.44249065417534E-15));
#42521=CARTESIAN_POINT('Ctrl Pts',(-8.76621624622179,12.3467783236356,0.130666807305558));
#42522=CARTESIAN_POINT('Ctrl Pts',(-8.77169236507929,12.3428956683044,0.261069786498707));
#42523=CARTESIAN_POINT('Ctrl Pts',(-8.78256611126601,12.3351536167882,0.390710450871087));
#42524=CARTESIAN_POINT('Ctrl Pts',(-8.79357042167237,12.3273186042172,0.521907748246256));
#42525=CARTESIAN_POINT('Ctrl Pts',(-8.8101027782242,12.315530900308,0.652324314224256));
#42526=CARTESIAN_POINT('Ctrl Pts',(-8.83205039902736,12.2997710546807,0.781443489202971));
#42527=CARTESIAN_POINT('Ctrl Pts',(-8.84930597782606,12.2873804060307,0.882959098491573));
#42528=CARTESIAN_POINT('Ctrl Pts',(-8.86990830867396,12.2725335396739,0.983672743459536));
#42529=CARTESIAN_POINT('Ctrl Pts',(-8.89378902201696,12.2552029391753,1.08333333333333));
#42530=CARTESIAN_POINT('Origin',(-11.1410986251694,8.88472967648693,9.85584169237584E-16));
#42531=CARTESIAN_POINT('',(-13.6377879061429,6.58029051604744,1.08333333333333));
#42532=CARTESIAN_POINT('',(-13.2594869773434,6.22835470309403,1.08333333333333));
#42533=CARTESIAN_POINT('Origin',(-11.1410986251694,8.88472967648693,1.08333333333333));
#42534=CARTESIAN_POINT('',(-13.6377879061429,6.58029051604744,-1.08333333333333));
#42535=CARTESIAN_POINT('Ctrl Pts',(-13.6377879061429,6.58029051604746,-1.08333333333332));
#42536=CARTESIAN_POINT('Ctrl Pts',(-13.6907677796516,6.47048863474076,-0.727666221822785));
#42537=CARTESIAN_POINT('Ctrl Pts',(-13.7154355939007,6.41687686636447,-0.35278297384277));
#42538=CARTESIAN_POINT('Ctrl Pts',(-13.7154355939007,6.41687686636447,0.352782973842772));
#42539=CARTESIAN_POINT('Ctrl Pts',(-13.6907677796516,6.47048863474076,0.727666221822785));
#42540=CARTESIAN_POINT('Ctrl Pts',(-13.6377879061429,6.58029051604746,1.08333333333332));
#42541=CARTESIAN_POINT('',(-12.9276994994136,5.99475484510091,-1.08333333333333));
#42542=CARTESIAN_POINT('Origin',(-11.1410986251694,8.88472967648693,-1.08333333333333));
#42543=CARTESIAN_POINT('',(-12.9276994994136,5.99475484510091,1.08333333333333));
#42544=CARTESIAN_POINT('Ctrl Pts',(-12.9276994994136,5.99475484510092,1.08333333333333));
#42545=CARTESIAN_POINT('Ctrl Pts',(-12.9759843593574,5.89062845864246,0.725928647976576));
#42546=CARTESIAN_POINT('Ctrl Pts',(-12.9982133898606,5.84028669430256,0.352039859176989));
#42547=CARTESIAN_POINT('Ctrl Pts',(-12.9982133898606,5.84028669430256,-0.352039859176986));
#42548=CARTESIAN_POINT('Ctrl Pts',(-12.9759843593574,5.89062845864246,-0.725928647976575));
#42549=CARTESIAN_POINT('Ctrl Pts',(-12.9276994994136,5.99475484510092,-1.08333333333332));
#42550=CARTESIAN_POINT('Origin',(-11.1410986251694,8.88472967648693,1.08333333333333));
#42551=CARTESIAN_POINT('',(-9.02271027299537,11.5411046498798,1.08333333333333));
#42552=CARTESIAN_POINT('Origin',(-11.1410986251694,8.88472967648693,9.85584169237584E-16));
#42553=CARTESIAN_POINT('',(-8.72113759169224,11.2696166353063,1.08333333333333));
#42554=CARTESIAN_POINT('Origin',(-11.1410986251694,8.88472967648693,1.08333333333333));
#42555=CARTESIAN_POINT('',(-8.72113759169224,11.2696166353063,-1.08333333333333));
#42556=CARTESIAN_POINT('Ctrl Pts',(-8.72113759169222,11.2696166353063,-1.08333333333334));
#42557=CARTESIAN_POINT('Ctrl Pts',(-8.63036626326988,11.3398611937656,-0.725928647976585));
#42558=CARTESIAN_POINT('Ctrl Pts',(-8.58623309669495,11.3727349924818,-0.352039859176991));
#42559=CARTESIAN_POINT('Ctrl Pts',(-8.58623309669495,11.3727349924818,4.46574186955748E-16));
#42560=CARTESIAN_POINT('Ctrl Pts',(-8.58623309669495,11.3727349924818,0.352039859176991));
#42561=CARTESIAN_POINT('Ctrl Pts',(-8.63036626326988,11.3398611937656,0.725928647976585));
#42562=CARTESIAN_POINT('Ctrl Pts',(-8.72113759169222,11.2696166353063,1.08333333333334));
#42563=CARTESIAN_POINT('',(-9.45000219633307,11.8316076987796,-1.08333333333333));
#42564=CARTESIAN_POINT('Origin',(-11.1410986251694,8.88472967648693,-1.08333333333333));
#42565=CARTESIAN_POINT('',(-9.45000219633307,11.8316076987796,1.08333333333333));
#42566=CARTESIAN_POINT('Ctrl Pts',(-9.45000219633306,11.8316076987796,1.08333333333334));
#42567=CARTESIAN_POINT('Ctrl Pts',(-9.35474240837113,11.9076924734257,0.727666221822798));
#42568=CARTESIAN_POINT('Ctrl Pts',(-9.30796390402501,11.9436715548398,0.352782973842778));
#42569=CARTESIAN_POINT('Ctrl Pts',(-9.30796390402501,11.9436715548398,5.10741104345864E-16));
#42570=CARTESIAN_POINT('Ctrl Pts',(-9.30796390402501,11.9436715548398,-0.352782973842777));
#42571=CARTESIAN_POINT('Ctrl Pts',(-9.35474240837113,11.9076924734257,-0.727666221822798));
#42572=CARTESIAN_POINT('Ctrl Pts',(-9.45000219633306,11.8316076987796,-1.08333333333334));
#42573=CARTESIAN_POINT('Origin',(-11.1410986251694,8.88472967648693,1.08333333333333));
#42574=CARTESIAN_POINT('',(-10.4434643792749,8.32838493021299,-3.45272288248773));
#42575=CARTESIAN_POINT('Origin',(-10.4434643792749,8.32838493021299,9.23868777263733E-16));
#42576=CARTESIAN_POINT('',(-11.838732871064,9.44107442276088,-3.45272288248773));
#42577=CARTESIAN_POINT('Origin',(-11.838732871064,9.44107442276088,1.04729956121144E-15));
#42578=CARTESIAN_POINT('Origin',(-13.892722748591,-3.17092330887753,3.20017169526126E-15));
#42579=CARTESIAN_POINT('',(-14.7626584240763,-3.36948044994625,3.96060240207311));
#42580=CARTESIAN_POINT('Origin',(-14.7626584240763,-3.36948044994625,3.40056031423578E-15));
#42581=CARTESIAN_POINT('',(-13.0227870731057,-2.97236616780882,3.96060240207311));
#42582=CARTESIAN_POINT('Origin',(-13.892722748591,-3.17092330887753,2.5198520116158));
#42583=CARTESIAN_POINT('Origin',(-13.0227870731057,-2.97236616780882,2.99978307628674E-15));
#42584=CARTESIAN_POINT('',(-12.4579905368413,-6.91816245718267,-1.08333333333333));
#42585=CARTESIAN_POINT('',(-13.3303603014234,-7.18268588222789,-1.08333333333333));
#42586=CARTESIAN_POINT('Ctrl Pts',(-12.4579905368413,-6.91816245718265,
-1.08333333333333));
#42587=CARTESIAN_POINT('Ctrl Pts',(-12.6155690741986,-7.02043310055334,
-1.08333333333333));
#42588=CARTESIAN_POINT('Ctrl Pts',(-12.8106483205941,-7.10161932916232,
-1.08333333333333));
#42589=CARTESIAN_POINT('Ctrl Pts',(-13.0926472341269,-7.16598374096129,
-1.08333333333333));
#42590=CARTESIAN_POINT('Ctrl Pts',(-13.211632620936,-7.18117853359748,-1.08333333333333));
#42591=CARTESIAN_POINT('Ctrl Pts',(-13.3303603014234,-7.18268588222786,
-1.08333333333333));
#42592=CARTESIAN_POINT('',(-13.3303603014234,-7.18268588222787,1.08333333333334));
#42593=CARTESIAN_POINT('Ctrl Pts',(-13.3303603014234,-7.18268588222788,
1.08333333333333));
#42594=CARTESIAN_POINT('Ctrl Pts',(-13.312602432605,-7.21564274452362,0.9568886321034));
#42595=CARTESIAN_POINT('Ctrl Pts',(-13.2978764135175,-7.24268913148589,
0.828820583351364));
#42596=CARTESIAN_POINT('Ctrl Pts',(-13.2863164700111,-7.26383348564883,
0.699646919262042));
#42597=CARTESIAN_POINT('Ctrl Pts',(-13.2748173090022,-7.28486666222222,
0.571152453813466));
#42598=CARTESIAN_POINT('Ctrl Pts',(-13.2664510227833,-7.30005980724142,
0.441563969171881));
#42599=CARTESIAN_POINT('Ctrl Pts',(-13.2613042752926,-7.30939745578436,
0.311391073638092));
#42600=CARTESIAN_POINT('Ctrl Pts',(-13.2561988309335,-7.3186601688214,0.182262827807686));
#42601=CARTESIAN_POINT('Ctrl Pts',(-13.2542614634094,-7.32216103446744,
0.0525595133522827));
#42602=CARTESIAN_POINT('Ctrl Pts',(-13.2555318677528,-7.31986045983868,
-0.0772214321944347));
#42603=CARTESIAN_POINT('Ctrl Pts',(-13.2563983335701,-7.31829137729732,
-0.165737150534351));
#42604=CARTESIAN_POINT('Ctrl Pts',(-13.2587560588234,-7.31402308269238,
-0.254288981130211));
#42605=CARTESIAN_POINT('Ctrl Pts',(-13.2626054360146,-7.30703628683457,
-0.342719102199554));
#42606=CARTESIAN_POINT('Ctrl Pts',(-13.2684086950193,-7.29650310602083,
-0.476034927301584));
#42607=CARTESIAN_POINT('Ctrl Pts',(-13.2775701666804,-7.27985434187078,
-0.608312350205395));
#42608=CARTESIAN_POINT('Ctrl Pts',(-13.2899434176249,-7.25719547792734,
-0.739057191237093));
#42609=CARTESIAN_POINT('Ctrl Pts',(-13.3009290370229,-7.23707775329796,
-0.855139299993907));
#42610=CARTESIAN_POINT('Ctrl Pts',(-13.3144456587151,-7.21222189770289,
-0.970013302477609));
#42611=CARTESIAN_POINT('Ctrl Pts',(-13.3303603014234,-7.18268588222788,
-1.08333333333332));
#42612=CARTESIAN_POINT('',(-12.4579905368413,-6.91816245718267,1.08333333333334));
#42613=CARTESIAN_POINT('Ctrl Pts',(-12.4579905368413,-6.91816245718265,
1.08333333333333));
#42614=CARTESIAN_POINT('Ctrl Pts',(-12.6150882655077,-7.02012104908378,
1.08333333333333));
#42615=CARTESIAN_POINT('Ctrl Pts',(-12.8106174809568,-7.10161229021636,
1.08333333333333));
#42616=CARTESIAN_POINT('Ctrl Pts',(-13.0925863122299,-7.16596983593587,
1.08333333333333));
#42617=CARTESIAN_POINT('Ctrl Pts',(-13.2116839714656,-7.18117918553602,
1.08333333333333));
#42618=CARTESIAN_POINT('Ctrl Pts',(-13.3303603014234,-7.18268588222786,
1.08333333333333));
#42619=CARTESIAN_POINT('Ctrl Pts',(-12.4579905368413,-6.91816245718269,
-1.08333333333333));
#42620=CARTESIAN_POINT('Ctrl Pts',(-12.4412857888864,-6.94824379644449,
-0.949270311030495));
#42621=CARTESIAN_POINT('Ctrl Pts',(-12.4276027080703,-6.97263587945683,
-0.813521288368019));
#42622=CARTESIAN_POINT('Ctrl Pts',(-12.4170780656485,-6.99132836531023,
-0.676607052101084));
#42623=CARTESIAN_POINT('Ctrl Pts',(-12.4080806643214,-7.0073083663671,-0.559560573777871));
#42624=CARTESIAN_POINT('Ctrl Pts',(-12.4013908554087,-7.01912257498617,
-0.441662516279072));
#42625=CARTESIAN_POINT('Ctrl Pts',(-12.3970674919579,-7.02675014497037,
-0.323238258334728));
#42626=CARTESIAN_POINT('Ctrl Pts',(-12.392071820683,-7.03556384585404,-0.186398348762656));
#42627=CARTESIAN_POINT('Ctrl Pts',(-12.3902516338786,-7.03876210460556,
-0.0492519096262199));
#42628=CARTESIAN_POINT('Ctrl Pts',(-12.3916053560034,-7.03637809537454,
0.0876758270660418));
#42629=CARTESIAN_POINT('Ctrl Pts',(-12.3929630026022,-7.03398717484178,
0.22500052065431));
#42630=CARTESIAN_POINT('Ctrl Pts',(-12.3975129673671,-7.02598155019929,
0.36210524191276));
#42631=CARTESIAN_POINT('Ctrl Pts',(-12.4052079364271,-7.0123687905019,0.498460177595606));
#42632=CARTESIAN_POINT('Ctrl Pts',(-12.4129361026924,-6.99869730339788,
0.635403368116707));
#42633=CARTESIAN_POINT('Ctrl Pts',(-12.4238364813948,-6.97937013765694,
0.771590289741313));
#42634=CARTESIAN_POINT('Ctrl Pts',(-12.4378151222667,-6.9543694886247,0.906484242526672));
#42635=CARTESIAN_POINT('Ctrl Pts',(-12.4439512822522,-6.94339503240897,
0.965698216399908));
#42636=CARTESIAN_POINT('Ctrl Pts',(-12.450680002204,-6.93132701813286,1.024663045654));
#42637=CARTESIAN_POINT('Ctrl Pts',(-12.4579905368413,-6.91816245718269,
1.08333333333334));
#42638=CARTESIAN_POINT('',(-15.1266902369927,0.68754979644356,-1.08333333333333));
#42639=CARTESIAN_POINT('',(-14.2259398250621,0.827729480997533,-1.08333333333333));
#42640=CARTESIAN_POINT('Ctrl Pts',(-15.1266902369927,0.687549796443589,
-1.08333333333333));
#42641=CARTESIAN_POINT('Ctrl Pts',(-15.0191128271494,0.737684039417719,
-1.08333333333333));
#42642=CARTESIAN_POINT('Ctrl Pts',(-14.905210454464,0.775655426636244,-1.08333333333333));
#42643=CARTESIAN_POINT('Ctrl Pts',(-14.6232416231909,0.840012972355744,
-1.08333333333333));
#42644=CARTESIAN_POINT('Ctrl Pts',(-14.411718162898,0.851428848194329,-1.08333333333333));
#42645=CARTESIAN_POINT('Ctrl Pts',(-14.2259398250622,0.827729480996923,
-1.08333333333333));
#42646=CARTESIAN_POINT('',(-14.2259398250711,0.827729480998061,1.08333333333334));
#42647=CARTESIAN_POINT('Ctrl Pts',(-14.2259398250621,0.827729480996948,
1.08333333333319));
#42648=CARTESIAN_POINT('Ctrl Pts',(-14.2239464151202,0.86198962338768,0.949622058007746));
#42649=CARTESIAN_POINT('Ctrl Pts',(-14.2222079250172,0.889808711690097,
0.814376693553578));
#42650=CARTESIAN_POINT('Ctrl Pts',(-14.2208398148552,0.911161325029729,
0.678132403728685));
#42651=CARTESIAN_POINT('Ctrl Pts',(-14.2194782068654,0.932412456504284,
0.542535637671376));
#42652=CARTESIAN_POINT('Ctrl Pts',(-14.2184834780892,0.947258512328182,
0.405949418799462));
#42653=CARTESIAN_POINT('Ctrl Pts',(-14.2179179597194,0.955671957675903,
0.268901316712362));
#42654=CARTESIAN_POINT('Ctrl Pts',(-14.2175487034788,0.961165532005871,
0.179415511019154));
#42655=CARTESIAN_POINT('Ctrl Pts',(-14.2173613909827,0.963916530719958,
0.0897327832368514));
#42656=CARTESIAN_POINT('Ctrl Pts',(-14.2173613909827,0.963916530719958,
-1.77635683940025E-15));
#42657=CARTESIAN_POINT('Ctrl Pts',(-14.2173613909827,0.963916530719959,
-0.137573936980362));
#42658=CARTESIAN_POINT('Ctrl Pts',(-14.2178040883167,0.957451598945575,
-0.274951212619699));
#42659=CARTESIAN_POINT('Ctrl Pts',(-14.2186598102071,0.944570379379332,
-0.411612406214706));
#42660=CARTESIAN_POINT('Ctrl Pts',(-14.2195221530139,0.931589494866292,
-0.549330978772852));
#42661=CARTESIAN_POINT('Ctrl Pts',(-14.2208039138492,0.912092599491199,
-0.686322345436968));
#42662=CARTESIAN_POINT('Ctrl Pts',(-14.222421741201,0.886126297665223,-0.82205493534731));
#42663=CARTESIAN_POINT('Ctrl Pts',(-14.2234666476786,0.869355437073727,
-0.909720570537294));
#42664=CARTESIAN_POINT('Ctrl Pts',(-14.2246506698206,0.849885807806941,
-0.996861109122796));
#42665=CARTESIAN_POINT('Ctrl Pts',(-14.2259398250621,0.827729480996951,
-1.08333333333318));
#42666=CARTESIAN_POINT('',(-15.1266902369927,0.687549796443561,1.08333333333334));
#42667=CARTESIAN_POINT('Ctrl Pts',(-15.1266902369927,0.687549796443589,
1.08333333333333));
#42668=CARTESIAN_POINT('Ctrl Pts',(-15.0191128271494,0.73768403941772,1.08333333333333));
#42669=CARTESIAN_POINT('Ctrl Pts',(-14.905210454464,0.775655426636245,1.08333333333333));
#42670=CARTESIAN_POINT('Ctrl Pts',(-14.6232416231937,0.840012972355103,
1.08333333333333));
#42671=CARTESIAN_POINT('Ctrl Pts',(-14.4117181629048,0.851428848194163,
1.08333333333333));
#42672=CARTESIAN_POINT('Ctrl Pts',(-14.2259398250711,0.827729480998062,
1.08333333333333));
#42673=CARTESIAN_POINT('Ctrl Pts',(-15.1266902369927,0.687549796443564,
-1.08333333333333));
#42674=CARTESIAN_POINT('Ctrl Pts',(-15.1249773086751,0.725235701077295,
-0.955915065626697));
#42675=CARTESIAN_POINT('Ctrl Pts',(-15.1234319803901,0.756223536825465,
-0.826701571450772));
#42676=CARTESIAN_POINT('Ctrl Pts',(-15.122183667988,0.780412301388329,-0.696211209492499));
#42677=CARTESIAN_POINT('Ctrl Pts',(-15.1209550316477,0.804219799510246,
-0.567777653525797));
#42678=CARTESIAN_POINT('Ctrl Pts',(-15.12001416535,0.821440959530219,-0.438107164856512));
#42679=CARTESIAN_POINT('Ctrl Pts',(-15.1194343523859,0.83197783168462,-0.307693975181787));
#42680=CARTESIAN_POINT('Ctrl Pts',(-15.1189800281283,0.840234212474348,
-0.205506064179395));
#42681=CARTESIAN_POINT('Ctrl Pts',(-15.1187464308798,0.844386527178334,
-0.102862147741089));
#42682=CARTESIAN_POINT('Ctrl Pts',(-15.1187464308798,0.844386527178334,
1.99840144432528E-15));
#42683=CARTESIAN_POINT('Ctrl Pts',(-15.1187464308798,0.844386527178334,
0.130666807305563));
#42684=CARTESIAN_POINT('Ctrl Pts',(-15.1191251529677,0.837684329050672,
0.261069786498716));
#42685=CARTESIAN_POINT('Ctrl Pts',(-15.1198518432089,0.824355801783686,
0.3907104508711));
#42686=CARTESIAN_POINT('Ctrl Pts',(-15.1205872590302,0.810867235029684,
0.521907748246278));
#42687=CARTESIAN_POINT('Ctrl Pts',(-15.1216790167187,0.790592205023353,
0.652324314224286));
#42688=CARTESIAN_POINT('Ctrl Pts',(-15.1230415909943,0.763606761086714,
0.78144348920301));
#42689=CARTESIAN_POINT('Ctrl Pts',(-15.1241128691977,0.742390363261972,
0.882959098491598));
#42690=CARTESIAN_POINT('Ctrl Pts',(-15.1253504648421,0.717025942629857,
0.983672743459549));
#42691=CARTESIAN_POINT('Ctrl Pts',(-15.1266902369927,0.687549796443564,
1.08333333333333));
#42692=CARTESIAN_POINT('Origin',(-13.892722748591,-3.17092330887753,3.20017169526126E-15));
#42693=CARTESIAN_POINT('',(-13.6476999686241,-6.55970790622096,1.08333333333334));
#42694=CARTESIAN_POINT('',(-13.1366786991091,-6.483368720524,1.08333333333334));
#42695=CARTESIAN_POINT('Origin',(-13.892722748591,-3.17092330887753,1.08333333333334));
#42696=CARTESIAN_POINT('',(-13.6476999686241,-6.55970790622096,-1.08333333333333));
#42697=CARTESIAN_POINT('Ctrl Pts',(-13.6476999686241,-6.55970790622096,
-1.08333333333332));
#42698=CARTESIAN_POINT('Ctrl Pts',(-13.5948858118208,-6.66958959248691,
-0.727666221822786));
#42699=CARTESIAN_POINT('Ctrl Pts',(-13.5683505740919,-6.72230205711272,
-0.35278297384277));
#42700=CARTESIAN_POINT('Ctrl Pts',(-13.5683505740919,-6.72230205711272,
0.352782973842779));
#42701=CARTESIAN_POINT('Ctrl Pts',(-13.5948858118208,-6.66958959248691,
0.727666221822796));
#42702=CARTESIAN_POINT('Ctrl Pts',(-13.6476999686241,-6.55970790622096,
1.08333333333333));
#42703=CARTESIAN_POINT('',(-12.7471768669563,-6.36961395396413,-1.08333333333333));
#42704=CARTESIAN_POINT('Origin',(-13.892722748591,-3.17092330887754,-1.08333333333333));
#42705=CARTESIAN_POINT('',(-12.7471768669563,-6.36961395396413,1.08333333333334));
#42706=CARTESIAN_POINT('Ctrl Pts',(-12.7471768669563,-6.36961395396412,
1.08333333333334));
#42707=CARTESIAN_POINT('Ctrl Pts',(-12.6958726976266,-6.472286317656,0.725928647976585));
#42708=CARTESIAN_POINT('Ctrl Pts',(-12.6703734952066,-6.52105325020167,
0.352039859176994));
#42709=CARTESIAN_POINT('Ctrl Pts',(-12.6703734952066,-6.52105325020167,
-0.352039859176985));
#42710=CARTESIAN_POINT('Ctrl Pts',(-12.6958726976266,-6.472286317656,-0.725928647976576));
#42711=CARTESIAN_POINT('Ctrl Pts',(-12.7471768669563,-6.36961395396413,
-1.08333333333333));
#42712=CARTESIAN_POINT('Origin',(-13.892722748591,-3.17092330887753,1.08333333333334));
#42713=CARTESIAN_POINT('',(-14.6487667980729,0.141522102768936,1.08333333333334));
#42714=CARTESIAN_POINT('Origin',(-13.892722748591,-3.17092330887753,3.20017169526126E-15));
#42715=CARTESIAN_POINT('',(-14.2484814298548,0.208031110850571,1.08333333333334));
#42716=CARTESIAN_POINT('Origin',(-13.892722748591,-3.17092330887753,1.08333333333334));
#42717=CARTESIAN_POINT('',(-14.2484814298548,0.20803111085057,-1.08333333333333));
#42718=CARTESIAN_POINT('Ctrl Pts',(-14.2484814298548,0.208031110850584,
-1.08333333333333));
#42719=CARTESIAN_POINT('Ctrl Pts',(-14.2468058395578,0.322795758952019,
-0.725928647976579));
#42720=CARTESIAN_POINT('Ctrl Pts',(-14.2449910310593,0.37779693624925,-0.352039859176988));
#42721=CARTESIAN_POINT('Ctrl Pts',(-14.2449910310593,0.37779693624925,2.46631154156404E-15));
#42722=CARTESIAN_POINT('Ctrl Pts',(-14.2449910310593,0.37779693624925,0.352039859176994));
#42723=CARTESIAN_POINT('Ctrl Pts',(-14.2468058395578,0.322795758952019,
0.725928647976587));
#42724=CARTESIAN_POINT('Ctrl Pts',(-14.2484814298548,0.208031110850583,
1.08333333333334));
#42725=CARTESIAN_POINT('',(-15.1423033840733,-0.0114224867028862,-1.08333333333333));
#42726=CARTESIAN_POINT('Origin',(-13.892722748591,-3.17092330887754,-1.08333333333333));
#42727=CARTESIAN_POINT('',(-15.1423033840733,-0.0114224867028857,1.08333333333334));
#42728=CARTESIAN_POINT('Ctrl Pts',(-15.1423033840733,-0.0114224867028744,
1.08333333333334));
#42729=CARTESIAN_POINT('Ctrl Pts',(-15.1423953499066,0.110492695607543,
0.727666221822802));
#42730=CARTESIAN_POINT('Ctrl Pts',(-15.1413590080604,0.169498193350012,
0.352782973842781));
#42731=CARTESIAN_POINT('Ctrl Pts',(-15.1413590080604,0.169498193350012,
2.67362166230902E-15));
#42732=CARTESIAN_POINT('Ctrl Pts',(-15.1413590080604,0.169498193350012,
-0.352782973842774));
#42733=CARTESIAN_POINT('Ctrl Pts',(-15.1423953499066,0.110492695607543,
-0.727666221822795));
#42734=CARTESIAN_POINT('Ctrl Pts',(-15.1423033840733,-0.0114224867028733,
-1.08333333333333));
#42735=CARTESIAN_POINT('Origin',(-13.892722748591,-3.17092330887753,1.08333333333334));
#42736=CARTESIAN_POINT('',(-13.0227870731057,-2.97236616780882,-3.45272288248773));
#42737=CARTESIAN_POINT('Origin',(-13.0227870731057,-2.97236616780882,2.99978307628674E-15));
#42738=CARTESIAN_POINT('',(-14.7626584240763,-3.36948044994625,-3.45272288248773));
#42739=CARTESIAN_POINT('Origin',(-14.7626584240763,-3.36948044994625,3.40056031423578E-15));
#42740=CARTESIAN_POINT('Origin',(-6.18284328242512,-12.8388063676095,4.97613300162231E-15));
#42741=CARTESIAN_POINT('',(-6.57000108040694,-13.6427478189686,3.96060240207311));
#42742=CARTESIAN_POINT('Origin',(-6.57000108040694,-13.6427478189686,5.28772891427451E-15));
#42743=CARTESIAN_POINT('',(-5.79568548444331,-12.0348649162504,3.96060240207311));
#42744=CARTESIAN_POINT('Origin',(-6.18284328242512,-12.8388063676095,2.51985201161581));
#42745=CARTESIAN_POINT('Origin',(-5.79568548444331,-12.0348649162504,4.66453708897012E-15));
#42746=CARTESIAN_POINT('',(-2.35859284151935,-14.0534529496467,-1.08333333333333));
#42747=CARTESIAN_POINT('',(-2.69569375163562,-14.9004267538186,-1.08333333333333));
#42748=CARTESIAN_POINT('Ctrl Pts',(-2.35859284151934,-14.0534529496467,
-1.08333333333333));
#42749=CARTESIAN_POINT('Ctrl Pts',(-2.37682723618162,-14.2398470420046,
-1.08333333333333));
#42750=CARTESIAN_POINT('Ctrl Pts',(-2.43502529011671,-14.4435268961719,
-1.08333333333332));
#42751=CARTESIAN_POINT('Ctrl Pts',(-2.56051322547963,-14.7041052789647,
-1.08333333333333));
#42752=CARTESIAN_POINT('Ctrl Pts',(-2.62287825309305,-14.806702452812,-1.08333333333333));
#42753=CARTESIAN_POINT('Ctrl Pts',(-2.69569375163558,-14.9004267538186,
-1.08333333333333));
#42754=CARTESIAN_POINT('',(-2.69569375163563,-14.9004267538187,1.08333333333334));
#42755=CARTESIAN_POINT('Ctrl Pts',(-2.69569375163559,-14.9004267538186,
1.08333333333335));
#42756=CARTESIAN_POINT('Ctrl Pts',(-2.65857154890325,-14.9071426748862,
0.955915065626573));
#42757=CARTESIAN_POINT('Ctrl Pts',(-2.628016775001,-14.9125315333598,0.826701571450498));
#42758=CARTESIAN_POINT('Ctrl Pts',(-2.60415669762586,-14.9166970252376,
0.696211209492072));
#42759=CARTESIAN_POINT('Ctrl Pts',(-2.58067270588166,-14.9207968600927,
0.567777653525379));
#42760=CARTESIAN_POINT('Ctrl Pts',(-2.56367395385075,-14.923711651889,0.438107164856101));
#42761=CARTESIAN_POINT('Ctrl Pts',(-2.55327224255806,-14.9254910506792,
0.307693975181385));
#42762=CARTESIAN_POINT('Ctrl Pts',(-2.54512176981446,-14.9268853348437,
0.205506064179128));
#42763=CARTESIAN_POINT('Ctrl Pts',(-2.54102158203148,-14.9275815713119,
0.102862147740959));
#42764=CARTESIAN_POINT('Ctrl Pts',(-2.54102158203148,-14.9275815713119,
4.44089209850063E-15));
#42765=CARTESIAN_POINT('Ctrl Pts',(-2.54102158203148,-14.9275815713119,
-0.130666807305524));
#42766=CARTESIAN_POINT('Ctrl Pts',(-2.54764001565181,-14.9264594186595,
-0.261069786498646));
#42767=CARTESIAN_POINT('Ctrl Pts',(-2.56079607270382,-14.9242020129234,
-0.390710450870999));
#42768=CARTESIAN_POINT('Ctrl Pts',(-2.57411009834303,-14.9219175018628,
-0.521907748246163));
#42769=CARTESIAN_POINT('Ctrl Pts',(-2.59411972995703,-14.9184702682937,
-0.652324314224157));
#42770=CARTESIAN_POINT('Ctrl Pts',(-2.62073179377387,-14.9137938537994,
-0.781443489202868));
#42771=CARTESIAN_POINT('Ctrl Pts',(-2.64165463403551,-14.9101171801624,
-0.882959098491507));
#42772=CARTESIAN_POINT('Ctrl Pts',(-2.66665850662476,-14.9056796321318,
-0.983672743459509));
#42773=CARTESIAN_POINT('Ctrl Pts',(-2.69569375163559,-14.9004267538186,
-1.08333333333334));
#42774=CARTESIAN_POINT('',(-2.35859284151935,-14.0534529496467,1.08333333333334));
#42775=CARTESIAN_POINT('Ctrl Pts',(-2.35859284151934,-14.0534529496467,
1.08333333333333));
#42776=CARTESIAN_POINT('Ctrl Pts',(-2.37688304383397,-14.2404175142851,
1.08333333333333));
#42777=CARTESIAN_POINT('Ctrl Pts',(-2.43503901504648,-14.4435553962822,
1.08333333333334));
#42778=CARTESIAN_POINT('Ctrl Pts',(-2.56054033827446,-14.7041615792632,
1.08333333333334));
#42779=CARTESIAN_POINT('Ctrl Pts',(-2.62284674626764,-14.8066618988743,
1.08333333333334));
#42780=CARTESIAN_POINT('Ctrl Pts',(-2.69569375163563,-14.9004267538187,
1.08333333333334));
#42781=CARTESIAN_POINT('Ctrl Pts',(-2.35859284151935,-14.0534529496467,
-1.08333333333333));
#42782=CARTESIAN_POINT('Ctrl Pts',(-2.32474809698527,-14.0591331175362,
-0.949622058007895));
#42783=CARTESIAN_POINT('Ctrl Pts',(-2.29723964086638,-14.0636285445206,
-0.814376693553736));
#42784=CARTESIAN_POINT('Ctrl Pts',(-2.27611794897253,-14.0670461391994,
-0.678132403728853));
#42785=CARTESIAN_POINT('Ctrl Pts',(-2.25509664145098,-14.0704474911881,
-0.542535637671543));
#42786=CARTESIAN_POINT('Ctrl Pts',(-2.24040145926613,-14.0727812605466,
-0.405949418799629));
#42787=CARTESIAN_POINT('Ctrl Pts',(-2.23207311688321,-14.0741020886196,
-0.268901316712528));
#42788=CARTESIAN_POINT('Ctrl Pts',(-2.22663511068775,-14.0749645256946,
-0.179415511019263));
#42789=CARTESIAN_POINT('Ctrl Pts',(-2.2239114043034,-14.075394064317,-0.0897327832369026));
#42790=CARTESIAN_POINT('Ctrl Pts',(-2.2239114043034,-14.075394064317,8.43769498715119E-15));
#42791=CARTESIAN_POINT('Ctrl Pts',(-2.2239114043034,-14.075394064317,0.137573936980349));
#42792=CARTESIAN_POINT('Ctrl Pts',(-2.23031275616482,-14.0743870796481,
0.274951212619667));
#42793=CARTESIAN_POINT('Ctrl Pts',(-2.24306143269717,-14.0723550057958,
0.411612406214657));
#42794=CARTESIAN_POINT('Ctrl Pts',(-2.25590874866049,-14.0703072093226,
0.549330978772813));
#42795=CARTESIAN_POINT('Ctrl Pts',(-2.27520203478074,-14.0672183663696,
0.68632234543694));
#42796=CARTESIAN_POINT('Ctrl Pts',(-2.30087730766032,-14.0630175856782,
0.822054935347292));
#42797=CARTESIAN_POINT('Ctrl Pts',(-2.31746020132759,-14.0603044266067,
0.909720570537337));
#42798=CARTESIAN_POINT('Ctrl Pts',(-2.33670515605249,-14.0571263627534,
0.996861109122898));
#42799=CARTESIAN_POINT('Ctrl Pts',(-2.35859284151935,-14.0534529496467,
1.08333333333334));
#42800=CARTESIAN_POINT('',(-9.96888517526507,-11.3978423664701,-1.08333333333333));
#42801=CARTESIAN_POINT('',(-9.516873369993,-10.6062067328295,-1.08333333333333));
#42802=CARTESIAN_POINT('Ctrl Pts',(-9.96888517526507,-11.3978423664701,
-1.08333333333333));
#42803=CARTESIAN_POINT('Ctrl Pts',(-9.94100828682427,-11.282476771434,-1.08333333333333));
#42804=CARTESIAN_POINT('Ctrl Pts',(-9.89967854500783,-11.1697495378475,
-1.08333333333333));
#42805=CARTESIAN_POINT('Ctrl Pts',(-9.77419060964491,-10.9091711550547,
-1.08333333333333));
#42806=CARTESIAN_POINT('Ctrl Pts',(-9.65123318042897,-10.7366777723525,
-1.08333333333333));
#42807=CARTESIAN_POINT('Ctrl Pts',(-9.51687336999256,-10.6062067328299,
-1.08333333333333));
#42808=CARTESIAN_POINT('',(-9.51687336999906,-10.6062067328363,1.08333333333334));
#42809=CARTESIAN_POINT('Ctrl Pts',(-9.51687336999256,-10.6062067328299,
1.08333333333319));
#42810=CARTESIAN_POINT('Ctrl Pts',(-9.54248335115827,-10.5832270800755,
0.949270311030248));
#42811=CARTESIAN_POINT('Ctrl Pts',(-9.56321910180067,-10.5644593135702,
0.813521288367661));
#42812=CARTESIAN_POINT('Ctrl Pts',(-9.57910097474595,-10.5500390764974,
0.676607052100613));
#42813=CARTESIAN_POINT('Ctrl Pts',(-9.59267821366648,-10.5377113740467,
0.559560573777554));
#42814=CARTESIAN_POINT('Ctrl Pts',(-9.6027075928823,-10.5285603838747,0.44166251627891));
#42815=CARTESIAN_POINT('Ctrl Pts',(-9.6091818848891,-10.5226481221753,0.323238258334718));
#42816=CARTESIAN_POINT('Ctrl Pts',(-9.61666296645239,-10.5158164698571,
0.186398348762648));
#42817=CARTESIAN_POINT('Ctrl Pts',(-9.61937600851194,-10.5133302394117,
0.0492519096262118));
#42818=CARTESIAN_POINT('Ctrl Pts',(-9.61735300288125,-10.5151805128572,
-0.08767582706605));
#42819=CARTESIAN_POINT('Ctrl Pts',(-9.61532413250719,-10.5170361502911,
-0.225000520654331));
#42820=CARTESIAN_POINT('Ctrl Pts',(-9.60853168799772,-10.5232534570122,
-0.362105241912796));
#42821=CARTESIAN_POINT('Ctrl Pts',(-9.59697252030892,-10.5337846211338,
-0.498460177595657));
#42822=CARTESIAN_POINT('Ctrl Pts',(-9.5853634847053,-10.5443612182148,-0.635403368116659));
#42823=CARTESIAN_POINT('Ctrl Pts',(-9.56894645381043,-10.5592890006364,
-0.771590289741169));
#42824=CARTESIAN_POINT('Ctrl Pts',(-9.54768316346852,-10.578480335569,-0.906484242526434));
#42825=CARTESIAN_POINT('Ctrl Pts',(-9.53834928383367,-10.5869046954593,
-0.965698216399696));
#42826=CARTESIAN_POINT('Ctrl Pts',(-9.52808112091929,-10.5961500981613,
-1.02466304565381));
#42827=CARTESIAN_POINT('Ctrl Pts',(-9.51687336999256,-10.6062067328299,
-1.08333333333318));
#42828=CARTESIAN_POINT('',(-9.96888517526507,-11.3978423664701,1.08333333333334));
#42829=CARTESIAN_POINT('Ctrl Pts',(-9.96888517526507,-11.3978423664701,
1.08333333333333));
#42830=CARTESIAN_POINT('Ctrl Pts',(-9.94100828682427,-11.282476771434,1.08333333333333));
#42831=CARTESIAN_POINT('Ctrl Pts',(-9.89967854500783,-11.1697495378475,
1.08333333333333));
#42832=CARTESIAN_POINT('Ctrl Pts',(-9.77419060964618,-10.9091711550573,
1.08333333333333));
#42833=CARTESIAN_POINT('Ctrl Pts',(-9.6512331804331,-10.7366777723579,1.08333333333333));
#42834=CARTESIAN_POINT('Ctrl Pts',(-9.51687336999908,-10.6062067328363,
1.08333333333333));
#42835=CARTESIAN_POINT('Ctrl Pts',(-9.96888517526508,-11.3978423664701,
-1.08333333333333));
#42836=CARTESIAN_POINT('Ctrl Pts',(-9.99706424266063,-11.3731961327199,
-0.956888632103256));
#42837=CARTESIAN_POINT('Ctrl Pts',(-10.020155672713,-11.3528209383891,-0.828820583351071));
#42838=CARTESIAN_POINT('Ctrl Pts',(-10.038197564346,-11.3368457653652,-0.699646919261599));
#42839=CARTESIAN_POINT('Ctrl Pts',(-10.0561445912219,-11.3209545902358,
-0.571152453812953));
#42840=CARTESIAN_POINT('Ctrl Pts',(-10.0690951385517,-11.3094172714603,
-0.441563969171296));
#42841=CARTESIAN_POINT('Ctrl Pts',(-10.0770534136919,-11.3023217413999,
-0.311391073637437));
#42842=CARTESIAN_POINT('Ctrl Pts',(-10.0849478229272,-11.2952831536342,
-0.182262827807044));
#42843=CARTESIAN_POINT('Ctrl Pts',(-10.0879298097314,-11.2926153440655,
-0.0525595133516554));
#42844=CARTESIAN_POINT('Ctrl Pts',(-10.0859696068728,-11.2943658227348,
0.0772214321950453));
#42845=CARTESIAN_POINT('Ctrl Pts',(-10.0846326712896,-11.2955597181575,
0.165737150534751));
#42846=CARTESIAN_POINT('Ctrl Pts',(-10.0809960349672,-11.2988081152181,
0.2542889811304));
#42847=CARTESIAN_POINT('Ctrl Pts',(-10.0750409796764,-11.304115688826,0.342719102199531));
#42848=CARTESIAN_POINT('Ctrl Pts',(-10.0660632343107,-11.3121173012435,
0.476034927301883));
#42849=CARTESIAN_POINT('Ctrl Pts',(-10.0518705086679,-11.3247537742305,
0.608312350206005));
#42850=CARTESIAN_POINT('Ctrl Pts',(-10.0325330571073,-11.3418588735079,
0.739057191238004));
#42851=CARTESIAN_POINT('Ctrl Pts',(-10.0153642561251,-11.3570456753652,
0.855139299994515));
#42852=CARTESIAN_POINT('Ctrl Pts',(-9.99413932000721,-11.3757543553326,
0.970013302477919));
#42853=CARTESIAN_POINT('Ctrl Pts',(-9.96888517526508,-11.3978423664701,
1.08333333333334));
#42854=CARTESIAN_POINT('Origin',(-6.18284328242512,-12.8388063676095,4.97613300162231E-15));
#42855=CARTESIAN_POINT('',(-3.38061559238688,-14.7601124814492,1.08333333333334));
#42856=CARTESIAN_POINT('',(-3.12168342103518,-14.3129832609672,1.08333333333334));
#42857=CARTESIAN_POINT('Origin',(-6.18284328242512,-12.8388063676095,1.08333333333334));
#42858=CARTESIAN_POINT('',(-3.38061559238688,-14.7601124814492,-1.08333333333333));
#42859=CARTESIAN_POINT('Ctrl Pts',(-3.38061559238688,-14.7601124814492,
-1.08333333333333));
#42860=CARTESIAN_POINT('Ctrl Pts',(-3.26177754255684,-14.7873308217382,
-0.727666221822789));
#42861=CARTESIAN_POINT('Ctrl Pts',(-3.20402082808,-14.799450421612,-0.35278297384277));
#42862=CARTESIAN_POINT('Ctrl Pts',(-3.20402082808,-14.799450421612,0.352782973842781));
#42863=CARTESIAN_POINT('Ctrl Pts',(-3.26177754255684,-14.7873308217382,
0.727666221822798));
#42864=CARTESIAN_POINT('Ctrl Pts',(-3.38061559238688,-14.7601124814492,
1.08333333333334));
#42865=CARTESIAN_POINT('',(-2.96777005865995,-13.9375335292483,-1.08333333333333));
#42866=CARTESIAN_POINT('Origin',(-6.18284328242512,-12.8388063676095,-1.08333333333333));
#42867=CARTESIAN_POINT('',(-2.96777005865995,-13.9375335292483,1.08333333333334));
#42868=CARTESIAN_POINT('Ctrl Pts',(-2.96777005865994,-13.9375335292483,
1.08333333333334));
#42869=CARTESIAN_POINT('Ctrl Pts',(-2.85550994597631,-13.9614374861791,
0.725928647976589));
#42870=CARTESIAN_POINT('Ctrl Pts',(-2.80148393014434,-13.9719070920595,
0.352039859176996));
#42871=CARTESIAN_POINT('Ctrl Pts',(-2.80148393014434,-13.9719070920595,
-0.352039859176986));
#42872=CARTESIAN_POINT('Ctrl Pts',(-2.85550994597631,-13.9614374861791,
-0.725928647976579));
#42873=CARTESIAN_POINT('Ctrl Pts',(-2.96777005865994,-13.9375335292483,
-1.08333333333333));
#42874=CARTESIAN_POINT('Origin',(-6.18284328242512,-12.8388063676095,1.08333333333334));
#42875=CARTESIAN_POINT('',(-9.24400314381506,-11.3646294742518,1.08333333333334));
#42876=CARTESIAN_POINT('Origin',(-6.18284328242512,-12.8388063676095,4.97613300162231E-15));
#42877=CARTESIAN_POINT('',(-9.04642813528379,-11.0102060831369,1.08333333333334));
#42878=CARTESIAN_POINT('Origin',(-6.18284328242512,-12.8388063676095,1.08333333333334));
#42879=CARTESIAN_POINT('',(-9.04642813528379,-11.0102060831369,-1.08333333333333));
#42880=CARTESIAN_POINT('Ctrl Pts',(-9.0464281352838,-11.0102060831369,-1.08333333333332));
#42881=CARTESIAN_POINT('Ctrl Pts',(-9.13511003678158,-10.9373414661859,
-0.725928647976569));
#42882=CARTESIAN_POINT('Ctrl Pts',(-9.17698017417422,-10.901629918632,-0.352039859176982));
#42883=CARTESIAN_POINT('Ctrl Pts',(-9.17698017417422,-10.901629918632,4.5383086406711E-15));
#42884=CARTESIAN_POINT('Ctrl Pts',(-9.17698017417422,-10.901629918632,0.352039859176991));
#42885=CARTESIAN_POINT('Ctrl Pts',(-9.13511003678158,-10.9373414661859,
0.725928647976579));
#42886=CARTESIAN_POINT('Ctrl Pts',(-9.0464281352838,-11.0102060831369,1.08333333333333));
#42887=CARTESIAN_POINT('',(-9.43214127690829,-11.8458513067218,-1.08333333333333));
#42888=CARTESIAN_POINT('Origin',(-6.18284328242512,-12.8388063676095,-1.08333333333333));
#42889=CARTESIAN_POINT('',(-9.43214127690829,-11.8458513067218,1.08333333333334));
#42890=CARTESIAN_POINT('Ctrl Pts',(-9.43214127690829,-11.8458513067218,
1.08333333333333));
#42891=CARTESIAN_POINT('Ctrl Pts',(-9.52751574438859,-11.7699103356433,
0.727666221822793));
#42892=CARTESIAN_POINT('Ctrl Pts',(-9.57300195158999,-11.7323107648653,
0.352782973842778));
#42893=CARTESIAN_POINT('Ctrl Pts',(-9.57300195158999,-11.7323107648653,
4.85994849902029E-15));
#42894=CARTESIAN_POINT('Ctrl Pts',(-9.57300195158999,-11.7323107648653,
-0.352782973842768));
#42895=CARTESIAN_POINT('Ctrl Pts',(-9.52751574438859,-11.7699103356433,
-0.727666221822784));
#42896=CARTESIAN_POINT('Ctrl Pts',(-9.43214127690829,-11.8458513067218,
-1.08333333333332));
#42897=CARTESIAN_POINT('Origin',(-6.18284328242512,-12.8388063676095,1.08333333333334));
#42898=CARTESIAN_POINT('',(-5.79568548444331,-12.0348649162504,-3.45272288248773));
#42899=CARTESIAN_POINT('Origin',(-5.79568548444331,-12.0348649162504,4.66453708897012E-15));
#42900=CARTESIAN_POINT('',(-6.57000108040694,-13.6427478189686,-3.45272288248772));
#42901=CARTESIAN_POINT('Origin',(-6.57000108040694,-13.6427478189686,5.28772891427451E-15));
#42902=CARTESIAN_POINT('Origin',(6.1828432824253,-12.8388063676094,4.9761330016223E-15));
#42903=CARTESIAN_POINT('',(6.57000108040713,-13.6427478189685,3.96060240207311));
#42904=CARTESIAN_POINT('Origin',(6.57000108040713,-13.6427478189685,5.28772891427449E-15));
#42905=CARTESIAN_POINT('',(5.79568548444348,-12.0348649162503,3.96060240207311));
#42906=CARTESIAN_POINT('Origin',(6.1828432824253,-12.8388063676094,2.51985201161581));
#42907=CARTESIAN_POINT('Origin',(5.79568548444348,-12.0348649162504,4.66453708897011E-15));
#42908=CARTESIAN_POINT('',(9.51687336999268,-10.6062067328298,-1.08333333333333));
#42909=CARTESIAN_POINT('',(9.96888517526453,-11.3978423664706,-1.08333333333333));
#42910=CARTESIAN_POINT('Ctrl Pts',(9.5168733699927,-10.6062067328298,-1.08333333333333));
#42911=CARTESIAN_POINT('Ctrl Pts',(9.65164439811578,-10.737077088181,-1.08333333333333));
#42912=CARTESIAN_POINT('Ctrl Pts',(9.77420433457484,-10.9091996551649,-1.08333333333333));
#42913=CARTESIAN_POINT('Ctrl Pts',(9.89970565780286,-11.169805838146,-1.08333333333333));
#42914=CARTESIAN_POINT('Ctrl Pts',(9.94099622466366,-11.2824268534395,-1.08333333333333));
#42915=CARTESIAN_POINT('Ctrl Pts',(9.96888517526534,-11.3978423664704,-1.08333333333333));
#42916=CARTESIAN_POINT('',(9.9688851752657,-11.3978423664719,1.08333333333334));
#42917=CARTESIAN_POINT('Ctrl Pts',(9.96888517526519,-11.39784236647,1.08333333333359));
#42918=CARTESIAN_POINT('Ctrl Pts',(9.99728120861575,-11.3730063679711,0.955915065626921));
#42919=CARTESIAN_POINT('Ctrl Pts',(10.0205449777511,-11.3524775820965,0.826701571450959));
#42920=CARTESIAN_POINT('Ctrl Pts',(10.038678205356,-11.3364201641361,0.696211209492648));
#42921=CARTESIAN_POINT('Ctrl Pts',(10.0565256146782,-11.3206158452779,0.567777653525928));
#42922=CARTESIAN_POINT('Ctrl Pts',(10.0694030392049,-11.309143028737,0.438107164856624));
#42923=CARTESIAN_POINT('Ctrl Pts',(10.0772795901119,-11.3021200803759,0.307693975181881));
#42924=CARTESIAN_POINT('Ctrl Pts',(10.0834514220032,-11.2966171061454,0.20550606417946));
#42925=CARTESIAN_POINT('Ctrl Pts',(10.0865521868617,-11.2938455465903,0.102862147741125));
#42926=CARTESIAN_POINT('Ctrl Pts',(10.0865521868617,-11.2938455465903,4.44089209850063E-15));
#42927=CARTESIAN_POINT('Ctrl Pts',(10.0865521868617,-11.2938455465903,-0.130666807305562));
#42928=CARTESIAN_POINT('Ctrl Pts',(10.0815483267233,-11.2983203956244,-0.261069786498721));
#42929=CARTESIAN_POINT('Ctrl Pts',(10.0715807484455,-11.3071987457576,-0.390710450871112));
#42930=CARTESIAN_POINT('Ctrl Pts',(10.0614934865685,-11.3161837008123,-0.521907748246463));
#42931=CARTESIAN_POINT('Ctrl Pts',(10.0463225295865,-11.3296785457857,-0.652324314224642));
#42932=CARTESIAN_POINT('Ctrl Pts',(10.0260740111135,-11.3475689983448,-0.781443489203535));
#42933=CARTESIAN_POINT('Ctrl Pts',(10.0101542943843,-11.3616347650465,-0.88295909849203));
#42934=CARTESIAN_POINT('Ctrl Pts',(9.99109522006272,-11.3784168138781,-0.983672743459888));
#42935=CARTESIAN_POINT('Ctrl Pts',(9.96888517526519,-11.39784236647,-1.08333333333358));
#42936=CARTESIAN_POINT('',(9.51687336999268,-10.6062067328298,1.08333333333334));
#42937=CARTESIAN_POINT('Ctrl Pts',(9.5168733699927,-10.6062067328298,1.08333333333333));
#42938=CARTESIAN_POINT('Ctrl Pts',(9.65123318042911,-10.7366777723523,1.08333333333333));
#42939=CARTESIAN_POINT('Ctrl Pts',(9.77419060964506,-10.9091711550545,1.08333333333333));
#42940=CARTESIAN_POINT('Ctrl Pts',(9.89967854500826,-11.1697495378479,1.08333333333333));
#42941=CARTESIAN_POINT('Ctrl Pts',(9.94100828682489,-11.2824767714351,1.08333333333333));
#42942=CARTESIAN_POINT('Ctrl Pts',(9.96888517526571,-11.3978423664719,1.08333333333333));
#42943=CARTESIAN_POINT('Ctrl Pts',(9.51687336999268,-10.6062067328298,-1.08333333333333));
#42944=CARTESIAN_POINT('Ctrl Pts',(9.54241615713793,-10.5832873727889,-0.949622058007762));
#42945=CARTESIAN_POINT('Ctrl Pts',(9.56308206533645,-10.5645832486408,-0.814376693553466));
#42946=CARTESIAN_POINT('Ctrl Pts',(9.5789232079445,-10.5502004803844,-0.678132403728444));
#42947=CARTESIAN_POINT('Ctrl Pts',(9.59468906287363,-10.5358860686389,-0.542535637671145));
#42948=CARTESIAN_POINT('Ctrl Pts',(9.60567597345963,-10.5258519939611,-0.405949418799242));
#42949=CARTESIAN_POINT('Ctrl Pts',(9.61190127497217,-10.5201641565229,-0.268901316712153));
#42950=CARTESIAN_POINT('Ctrl Pts',(9.61596609683434,-10.5164502727984,-0.179415511019018));
#42951=CARTESIAN_POINT('Ctrl Pts',(9.61800012680612,-10.5145886063487,-0.0897327832367887));
#42952=CARTESIAN_POINT('Ctrl Pts',(9.61800012680612,-10.5145886063487,-9.32587340685131E-15));
#42953=CARTESIAN_POINT('Ctrl Pts',(9.61800012680612,-10.5145886063487,0.137573936980381));
#42954=CARTESIAN_POINT('Ctrl Pts',(9.61322165688595,-10.5189655400926,0.274951212619743));
#42955=CARTESIAN_POINT('Ctrl Pts',(9.6036842477684,-10.5276658794419,0.411612406214774));
#42956=CARTESIAN_POINT('Ctrl Pts',(9.59407304553156,-10.5364335353099,0.54933097877281));
#42957=CARTESIAN_POINT('Ctrl Pts',(9.57962892372621,-10.5495917717182,0.686322345436814));
#42958=CARTESIAN_POINT('Ctrl Pts',(9.5603363503304,-10.5670463644555,0.822054935347047));
#42959=CARTESIAN_POINT('Ctrl Pts',(9.54787585206456,-10.5783197657831,0.909720570537174));
#42960=CARTESIAN_POINT('Ctrl Pts',(9.5333921086825,-10.5913845868635,0.996861109122817));
#42961=CARTESIAN_POINT('Ctrl Pts',(9.51687336999268,-10.6062067328298,1.08333333333334));
#42962=CARTESIAN_POINT('',(2.69569375163578,-14.9004267538186,-1.08333333333333));
#42963=CARTESIAN_POINT('',(2.35859284151893,-14.0534529496468,-1.08333333333333));
#42964=CARTESIAN_POINT('Ctrl Pts',(2.6956937516358,-14.9004267538186,-1.08333333333332));
#42965=CARTESIAN_POINT('Ctrl Pts',(2.62284674626782,-14.8066618988742,-1.08333333333332));
#42966=CARTESIAN_POINT('Ctrl Pts',(2.56054033827465,-14.7041615792632,-1.08333333333332));
#42967=CARTESIAN_POINT('Ctrl Pts',(2.4350390150467,-14.4435553962822,-1.08333333333332));
#42968=CARTESIAN_POINT('Ctrl Pts',(2.37688304383419,-14.2404175142851,-1.08333333333332));
#42969=CARTESIAN_POINT('Ctrl Pts',(2.35859284151955,-14.0534529496467,-1.08333333333332));
#42970=CARTESIAN_POINT('',(2.35859284152043,-14.0534529496557,1.08333333333334));
#42971=CARTESIAN_POINT('Ctrl Pts',(2.35859284151951,-14.0534529496467,1.08333333333319));
#42972=CARTESIAN_POINT('Ctrl Pts',(2.32465906345733,-14.0591480600448,0.949270311030372));
#42973=CARTESIAN_POINT('Ctrl Pts',(2.29705730368849,-14.0636584116899,0.813521288367913));
#42974=CARTESIAN_POINT('Ctrl Pts',(2.27588092254449,-14.0670844892038,0.676607052100994));
#42975=CARTESIAN_POINT('Ctrl Pts',(2.25777746665768,-14.0700134052785,0.55956057377781));
#42976=CARTESIAN_POINT('Ctrl Pts',(2.24436971878542,-14.0721491406499,0.441662516279038));
#42977=CARTESIAN_POINT('Ctrl Pts',(2.23571067141573,-14.073524711092,0.323238258334718));
#42978=CARTESIAN_POINT('Ctrl Pts',(2.2257050924945,-14.0751141906309,0.186398348762649));
#42979=CARTESIAN_POINT('Ctrl Pts',(2.22206972520347,-14.0756851929985,0.0492519096262131));
#42980=CARTESIAN_POINT('Ctrl Pts',(2.22477765061414,-14.0752571701311,-0.087675827066048));
#42981=CARTESIAN_POINT('Ctrl Pts',(2.22749342636756,-14.0748279064149,-0.225000520654297));
#42982=CARTESIAN_POINT('Ctrl Pts',(2.23658933237962,-14.0733937867901,-0.362105241912729));
#42983=CARTESIAN_POINT('Ctrl Pts',(2.25202995120888,-14.0709225390114,-0.498460177595558));
#42984=CARTESIAN_POINT('Ctrl Pts',(2.26753718309241,-14.0684406299137,-0.635403368116538));
#42985=CARTESIAN_POINT('Ctrl Pts',(2.28944404469282,-14.0649125984157,-0.771590289741026));
#42986=CARTESIAN_POINT('Ctrl Pts',(2.31770587921582,-14.0602538902201,-0.906484242526269));
#42987=CARTESIAN_POINT('Ctrl Pts',(2.33011188776182,-14.0582088717468,-0.965698216399587));
#42988=CARTESIAN_POINT('Ctrl Pts',(2.34374232952329,-14.0559453130119,-1.02466304565376));
#42989=CARTESIAN_POINT('Ctrl Pts',(2.35859284151951,-14.0534529496467,-1.08333333333318));
#42990=CARTESIAN_POINT('',(2.69569375163578,-14.9004267538186,1.08333333333334));
#42991=CARTESIAN_POINT('Ctrl Pts',(2.6956937516358,-14.9004267538186,1.08333333333334));
#42992=CARTESIAN_POINT('Ctrl Pts',(2.62284674626782,-14.8066618988742,1.08333333333334));
#42993=CARTESIAN_POINT('Ctrl Pts',(2.56054033827465,-14.7041615792632,1.08333333333334));
#42994=CARTESIAN_POINT('Ctrl Pts',(2.43503901504795,-14.4435553962848,1.08333333333334));
#42995=CARTESIAN_POINT('Ctrl Pts',(2.37688304383586,-14.2404175142916,1.08333333333334));
#42996=CARTESIAN_POINT('Ctrl Pts',(2.35859284152042,-14.0534529496557,1.08333333333334));
#42997=CARTESIAN_POINT('Ctrl Pts',(2.69569375163578,-14.9004267538186,-1.08333333333333));
#42998=CARTESIAN_POINT('Ctrl Pts',(2.65885518901859,-14.9070913604575,-0.956888632103347));
#42999=CARTESIAN_POINT('Ctrl Pts',(2.62852794948137,-14.9124412415715,-0.828820583351256));
#43000=CARTESIAN_POINT('Ctrl Pts',(2.60478912083403,-14.9165866029902,-0.699646919261879));
#43001=CARTESIAN_POINT('Ctrl Pts',(2.58117511159368,-14.9207101679857,-0.571152453813268));
#43002=CARTESIAN_POINT('Ctrl Pts',(2.56408033836306,-14.9236419130061,-0.441563969171648));
#43003=CARTESIAN_POINT('Ctrl Pts',(2.55357092618676,-14.9254399524253,-0.311391073637824));
#43004=CARTESIAN_POINT('Ctrl Pts',(2.54314585302948,-14.9272235624095,-0.182262827807427));
#43005=CARTESIAN_POINT('Ctrl Pts',(2.53920083715778,-14.927891621514,-0.0525595133520343));
#43006=CARTESIAN_POINT('Ctrl Pts',(2.54179158298272,-14.9274504788058,0.077221432194672));
#43007=CARTESIAN_POINT('Ctrl Pts',(2.54355857371286,-14.9271496020974,0.165737150534507));
#43008=CARTESIAN_POINT('Ctrl Pts',(2.54836567846244,-14.9263317077699,0.254288981130285));
#43009=CARTESIAN_POINT('Ctrl Pts',(2.55622822284789,-14.9249850760809,0.342719102199546));
#43010=CARTESIAN_POINT('Ctrl Pts',(2.56808166802554,-14.9229549158531,0.47603492730158));
#43011=CARTESIAN_POINT('Ctrl Pts',(2.58681028013297,-14.9197373081624,0.608312350205393));
#43012=CARTESIAN_POINT('Ctrl Pts',(2.61224028910069,-14.9152835347009,0.739057191237091));
#43013=CARTESIAN_POINT('Ctrl Pts',(2.63481838123332,-14.9113292416576,0.855139299993913));
#43014=CARTESIAN_POINT('Ctrl Pts',(2.66267894744191,-14.9063995895532,0.970013302477622));
#43015=CARTESIAN_POINT('Ctrl Pts',(2.69569375163578,-14.9004267538186,1.08333333333334));
#43016=CARTESIAN_POINT('Origin',(6.1828432824253,-12.8388063676094,4.9761330016223E-15));
#43017=CARTESIAN_POINT('',(9.43214127690845,-11.8458513067217,1.08333333333334));
#43018=CARTESIAN_POINT('',(9.24400314381522,-11.3646294742516,1.08333333333334));
#43019=CARTESIAN_POINT('Origin',(6.1828432824253,-12.8388063676094,1.08333333333334));
#43020=CARTESIAN_POINT('',(9.43214127690845,-11.8458513067217,-1.08333333333333));
#43021=CARTESIAN_POINT('Ctrl Pts',(9.43214127690846,-11.8458513067217,-1.08333333333333));
#43022=CARTESIAN_POINT('Ctrl Pts',(9.52751574438875,-11.7699103356432,-0.727666221822791));
#43023=CARTESIAN_POINT('Ctrl Pts',(9.57300195159016,-11.7323107648652,-0.352782973842771));
#43024=CARTESIAN_POINT('Ctrl Pts',(9.57300195159016,-11.7323107648652,0.35278297384278));
#43025=CARTESIAN_POINT('Ctrl Pts',(9.52751574438876,-11.7699103356432,0.7276662218228));
#43026=CARTESIAN_POINT('Ctrl Pts',(9.43214127690846,-11.8458513067217,1.08333333333334));
#43027=CARTESIAN_POINT('',(9.04642813528394,-11.0102060831368,-1.08333333333333));
#43028=CARTESIAN_POINT('Origin',(6.1828432824253,-12.8388063676094,-1.08333333333333));
#43029=CARTESIAN_POINT('',(9.04642813528394,-11.0102060831368,1.08333333333334));
#43030=CARTESIAN_POINT('Ctrl Pts',(9.04642813528396,-11.0102060831368,1.08333333333334));
#43031=CARTESIAN_POINT('Ctrl Pts',(9.13511003678174,-10.9373414661857,0.725928647976586));
#43032=CARTESIAN_POINT('Ctrl Pts',(9.17698017417438,-10.9016299186319,0.352039859176995));
#43033=CARTESIAN_POINT('Ctrl Pts',(9.17698017417438,-10.9016299186319,-0.352039859176985));
#43034=CARTESIAN_POINT('Ctrl Pts',(9.13511003678174,-10.9373414661857,-0.725928647976577));
#43035=CARTESIAN_POINT('Ctrl Pts',(9.04642813528395,-11.0102060831368,-1.08333333333333));
#43036=CARTESIAN_POINT('Origin',(6.1828432824253,-12.8388063676094,1.08333333333334));
#43037=CARTESIAN_POINT('',(3.12168342103538,-14.3129832609672,1.08333333333334));
#43038=CARTESIAN_POINT('Origin',(6.1828432824253,-12.8388063676094,4.9761330016223E-15));
#43039=CARTESIAN_POINT('',(2.96777005866014,-13.9375335292483,1.08333333333334));
#43040=CARTESIAN_POINT('Origin',(6.1828432824253,-12.8388063676094,1.08333333333334));
#43041=CARTESIAN_POINT('',(2.96777005866014,-13.9375335292483,-1.08333333333333));
#43042=CARTESIAN_POINT('Ctrl Pts',(2.96777005866014,-13.9375335292483,-1.08333333333333));
#43043=CARTESIAN_POINT('Ctrl Pts',(2.85550994597651,-13.9614374861791,-0.725928647976576));
#43044=CARTESIAN_POINT('Ctrl Pts',(2.80148393014454,-13.9719070920595,-0.352039859176985));
#43045=CARTESIAN_POINT('Ctrl Pts',(2.80148393014454,-13.9719070920595,5.10230940761107E-15));
#43046=CARTESIAN_POINT('Ctrl Pts',(2.80148393014454,-13.9719070920595,0.352039859176993));
#43047=CARTESIAN_POINT('Ctrl Pts',(2.85550994597651,-13.9614374861791,0.725928647976584));
#43048=CARTESIAN_POINT('Ctrl Pts',(2.96777005866014,-13.9375335292483,1.08333333333333));
#43049=CARTESIAN_POINT('',(3.38061559238708,-14.7601124814491,-1.08333333333333));
#43050=CARTESIAN_POINT('Origin',(6.1828432824253,-12.8388063676094,-1.08333333333333));
#43051=CARTESIAN_POINT('',(3.38061559238708,-14.7601124814491,1.08333333333334));
#43052=CARTESIAN_POINT('Ctrl Pts',(3.3806155923871,-14.7601124814491,1.08333333333334));
#43053=CARTESIAN_POINT('Ctrl Pts',(3.26177754255705,-14.7873308217381,0.727666221822799));
#43054=CARTESIAN_POINT('Ctrl Pts',(3.20402082808022,-14.7994504216119,0.35278297384278));
#43055=CARTESIAN_POINT('Ctrl Pts',(3.20402082808022,-14.7994504216119,5.42337291349619E-15));
#43056=CARTESIAN_POINT('Ctrl Pts',(3.20402082808022,-14.7994504216119,-0.35278297384277));
#43057=CARTESIAN_POINT('Ctrl Pts',(3.26177754255705,-14.7873308217381,-0.727666221822788));
#43058=CARTESIAN_POINT('Ctrl Pts',(3.3806155923871,-14.7601124814491,-1.08333333333333));
#43059=CARTESIAN_POINT('Origin',(6.1828432824253,-12.8388063676094,1.08333333333334));
#43060=CARTESIAN_POINT('',(5.79568548444348,-12.0348649162504,-3.45272288248773));
#43061=CARTESIAN_POINT('Origin',(5.79568548444348,-12.0348649162504,4.66453708897011E-15));
#43062=CARTESIAN_POINT('',(6.57000108040713,-13.6427478189685,-3.45272288248772));
#43063=CARTESIAN_POINT('Origin',(6.57000108040713,-13.6427478189685,5.28772891427449E-15));
#43064=CARTESIAN_POINT('Origin',(13.892722748591,-3.17092330887735,3.20017169526122E-15));
#43065=CARTESIAN_POINT('',(14.7626584240763,-3.36948044994605,3.96060240207311));
#43066=CARTESIAN_POINT('Origin',(14.7626584240763,-3.36948044994605,3.40056031423575E-15));
#43067=CARTESIAN_POINT('',(13.0227870731057,-2.97236616780864,3.96060240207311));
#43068=CARTESIAN_POINT('Origin',(13.892722748591,-3.17092330887735,2.5198520116158));
#43069=CARTESIAN_POINT('Origin',(13.0227870731057,-2.97236616780865,2.9997830762867E-15));
#43070=CARTESIAN_POINT('',(14.2259398250621,0.827729480997053,-1.08333333333333));
#43071=CARTESIAN_POINT('',(15.1266902369927,0.68754979644376,-1.08333333333333));
#43072=CARTESIAN_POINT('Ctrl Pts',(14.2259398250621,0.827729480997104,-1.08333333333333));
#43073=CARTESIAN_POINT('Ctrl Pts',(14.4122867506183,0.85150138178118,-1.08333333333333));
#43074=CARTESIAN_POINT('Ctrl Pts',(14.6232724628281,0.840005933409976,-1.08333333333333));
#43075=CARTESIAN_POINT('Ctrl Pts',(14.9052713763609,0.775641521611009,-1.08333333333333));
#43076=CARTESIAN_POINT('Ctrl Pts',(15.0190662790554,0.737705732201359,-1.08333333333333));
#43077=CARTESIAN_POINT('Ctrl Pts',(15.1266902369927,0.687549796443767,-1.08333333333333));
#43078=CARTESIAN_POINT('',(15.1266902369927,0.687549796443762,1.08333333333334));
#43079=CARTESIAN_POINT('Ctrl Pts',(15.1266902369927,0.687549796443768,1.08333333333334));
#43080=CARTESIAN_POINT('Ctrl Pts',(15.1249773086751,0.725235701077452,0.955915065626868));
#43081=CARTESIAN_POINT('Ctrl Pts',(15.1234319803901,0.756223536825589,0.826701571451108));
#43082=CARTESIAN_POINT('Ctrl Pts',(15.122183667988,0.780412301388443,0.696211209493001));
#43083=CARTESIAN_POINT('Ctrl Pts',(15.1209550316477,0.804219799510377,0.567777653526322));
#43084=CARTESIAN_POINT('Ctrl Pts',(15.12001416535,0.821440959530357,0.43810716485706));
#43085=CARTESIAN_POINT('Ctrl Pts',(15.1194343523859,0.831977831684773,0.307693975182356));
#43086=CARTESIAN_POINT('Ctrl Pts',(15.1189800281283,0.840234212474528,0.205506064179778));
#43087=CARTESIAN_POINT('Ctrl Pts',(15.1187464308798,0.844386527178536,0.102862147741283));
#43088=CARTESIAN_POINT('Ctrl Pts',(15.1187464308798,0.844386527178536,1.99840144432528E-15));
#43089=CARTESIAN_POINT('Ctrl Pts',(15.1187464308798,0.844386527178536,-0.130666807305585));
#43090=CARTESIAN_POINT('Ctrl Pts',(15.1191251529677,0.837684329050871,-0.261069786498764));
#43091=CARTESIAN_POINT('Ctrl Pts',(15.1198518432089,0.824355801783881,-0.390710450871172));
#43092=CARTESIAN_POINT('Ctrl Pts',(15.1205872590302,0.810867235029882,-0.521907748246314));
#43093=CARTESIAN_POINT('Ctrl Pts',(15.1216790167187,0.790592205023559,-0.652324314224285));
#43094=CARTESIAN_POINT('Ctrl Pts',(15.1230415909943,0.763606761086929,-0.781443489202972));
#43095=CARTESIAN_POINT('Ctrl Pts',(15.1241128691977,0.742390363262186,-0.882959098491574));
#43096=CARTESIAN_POINT('Ctrl Pts',(15.1253504648421,0.717025942630064,-0.983672743459537));
#43097=CARTESIAN_POINT('Ctrl Pts',(15.1266902369927,0.687549796443768,-1.08333333333333));
#43098=CARTESIAN_POINT('',(14.2259398250621,0.827729480997055,1.08333333333334));
#43099=CARTESIAN_POINT('Ctrl Pts',(14.2259398250621,0.827729480997104,1.08333333333333));
#43100=CARTESIAN_POINT('Ctrl Pts',(14.4122867506183,0.85150138178118,1.08333333333333));
#43101=CARTESIAN_POINT('Ctrl Pts',(14.6232724628281,0.840005933409977,1.08333333333333));
#43102=CARTESIAN_POINT('Ctrl Pts',(14.9052713763609,0.775641521611009,1.08333333333333));
#43103=CARTESIAN_POINT('Ctrl Pts',(15.0190662790554,0.73770573220136,1.08333333333333));
#43104=CARTESIAN_POINT('Ctrl Pts',(15.1266902369927,0.687549796443768,1.08333333333333));
#43105=CARTESIAN_POINT('Ctrl Pts',(14.2259398250621,0.8277294809971,-1.08333333333334));
#43106=CARTESIAN_POINT('Ctrl Pts',(14.2239464151202,0.861989623387911,-0.949622058007612));
#43107=CARTESIAN_POINT('Ctrl Pts',(14.2222079250172,0.889808711690379,-0.814376693553152));
#43108=CARTESIAN_POINT('Ctrl Pts',(14.2208398148552,0.911161325030034,-0.678132403727965));
#43109=CARTESIAN_POINT('Ctrl Pts',(14.2194782068654,0.932412456504566,-0.542535637670654));
#43110=CARTESIAN_POINT('Ctrl Pts',(14.2184834780892,0.947258512328438,-0.40594941879874));
#43111=CARTESIAN_POINT('Ctrl Pts',(14.2179179597194,0.955671957676133,-0.268901316711642));
#43112=CARTESIAN_POINT('Ctrl Pts',(14.2175487034788,0.961165532006069,-0.179415511018676));
#43113=CARTESIAN_POINT('Ctrl Pts',(14.2173613909827,0.963916530720146,-0.0897327832366183));
#43114=CARTESIAN_POINT('Ctrl Pts',(14.2173613909827,0.963916530720146,-1.06581410364015E-14));
#43115=CARTESIAN_POINT('Ctrl Pts',(14.2173613909827,0.963916530720146,0.13757393698032));
#43116=CARTESIAN_POINT('Ctrl Pts',(14.2178040883167,0.957451598945758,0.274951212619625));
#43117=CARTESIAN_POINT('Ctrl Pts',(14.2186598102071,0.944570379379524,0.411612406214599));
#43118=CARTESIAN_POINT('Ctrl Pts',(14.2195221530139,0.931589494866494,0.549330978772693));
#43119=CARTESIAN_POINT('Ctrl Pts',(14.2208039138492,0.912092599491427,0.686322345436757));
#43120=CARTESIAN_POINT('Ctrl Pts',(14.222421741201,0.886126297665472,0.822054935347047));
#43121=CARTESIAN_POINT('Ctrl Pts',(14.2234666476786,0.869355437073955,0.909720570537178));
#43122=CARTESIAN_POINT('Ctrl Pts',(14.2246506698206,0.849885807807131,0.996861109122824));
#43123=CARTESIAN_POINT('Ctrl Pts',(14.2259398250621,0.827729480997101,1.08333333333335));
#43124=CARTESIAN_POINT('',(13.3303603014235,-7.18268588222768,-1.08333333333333));
#43125=CARTESIAN_POINT('',(12.4579905368411,-6.91816245718305,-1.08333333333333));
#43126=CARTESIAN_POINT('Ctrl Pts',(13.3303603014235,-7.18268588222769,-1.08333333333333));
#43127=CARTESIAN_POINT('Ctrl Pts',(13.2116326209361,-7.18117853359731,-1.08333333333333));
#43128=CARTESIAN_POINT('Ctrl Pts',(13.0926472341269,-7.16598374096113,-1.08333333333333));
#43129=CARTESIAN_POINT('Ctrl Pts',(12.8106483205942,-7.10161932916216,-1.08333333333333));
#43130=CARTESIAN_POINT('Ctrl Pts',(12.6155690741987,-7.02043310055321,-1.08333333333333));
#43131=CARTESIAN_POINT('Ctrl Pts',(12.4579905368414,-6.91816245718254,-1.08333333333333));
#43132=CARTESIAN_POINT('',(12.4579905368491,-6.91816245718746,1.08333333333334));
#43133=CARTESIAN_POINT('Ctrl Pts',(12.4579905368414,-6.91816245718254,1.08333333333318));
#43134=CARTESIAN_POINT('Ctrl Pts',(12.4412857888865,-6.94824379644432,0.949270311030419));
#43135=CARTESIAN_POINT('Ctrl Pts',(12.4276027080704,-6.97263587945666,0.813521288368017));
#43136=CARTESIAN_POINT('Ctrl Pts',(12.4170780656486,-6.99132836531005,0.676607052101155));
#43137=CARTESIAN_POINT('Ctrl Pts',(12.4080806643215,-7.00730836636693,0.559560573777918));
#43138=CARTESIAN_POINT('Ctrl Pts',(12.4013908554088,-7.019122574986,0.441662516279092));
#43139=CARTESIAN_POINT('Ctrl Pts',(12.397067491958,-7.0267501449702,0.323238258334718));
#43140=CARTESIAN_POINT('Ctrl Pts',(12.3920718206831,-7.03556384585387,0.186398348762654));
#43141=CARTESIAN_POINT('Ctrl Pts',(12.3902516338787,-7.03876210460539,0.0492519096262223));
#43142=CARTESIAN_POINT('Ctrl Pts',(12.3916053560035,-7.03637809537437,-0.0876758270660355));
#43143=CARTESIAN_POINT('Ctrl Pts',(12.3929630026023,-7.03398717484161,-0.225000520654302));
#43144=CARTESIAN_POINT('Ctrl Pts',(12.3975129673672,-7.02598155019911,-0.362105241912753));
#43145=CARTESIAN_POINT('Ctrl Pts',(12.4052079364272,-7.01236879050172,-0.498460177595601));
#43146=CARTESIAN_POINT('Ctrl Pts',(12.4129361026925,-6.99869730339771,-0.635403368116608));
#43147=CARTESIAN_POINT('Ctrl Pts',(12.4238364813948,-6.9793701376568,-0.771590289741124));
#43148=CARTESIAN_POINT('Ctrl Pts',(12.4378151222668,-6.95436948862457,-0.906484242526394));
#43149=CARTESIAN_POINT('Ctrl Pts',(12.4439512822523,-6.94339503240884,-0.96569821639967));
#43150=CARTESIAN_POINT('Ctrl Pts',(12.4506800022041,-6.93132701813272,-1.0246630456538));
#43151=CARTESIAN_POINT('Ctrl Pts',(12.4579905368414,-6.91816245718254,-1.08333333333318));
#43152=CARTESIAN_POINT('',(13.3303603014235,-7.18268588222768,1.08333333333334));
#43153=CARTESIAN_POINT('Ctrl Pts',(13.3303603014235,-7.18268588222769,1.08333333333333));
#43154=CARTESIAN_POINT('Ctrl Pts',(13.2116326209361,-7.18117853359731,1.08333333333333));
#43155=CARTESIAN_POINT('Ctrl Pts',(13.0926472341269,-7.16598374096113,1.08333333333333));
#43156=CARTESIAN_POINT('Ctrl Pts',(12.810648320597,-7.10161932916281,1.08333333333333));
#43157=CARTESIAN_POINT('Ctrl Pts',(12.6155690742049,-7.020433100556,1.08333333333333));
#43158=CARTESIAN_POINT('Ctrl Pts',(12.4579905368491,-6.91816245718749,1.08333333333333));
#43159=CARTESIAN_POINT('Ctrl Pts',(13.3303603014235,-7.18268588222769,-1.08333333333333));
#43160=CARTESIAN_POINT('Ctrl Pts',(13.3126024326051,-7.21564274452345,-0.956888632103319));
#43161=CARTESIAN_POINT('Ctrl Pts',(13.2978764135175,-7.24268913148574,-0.828820583351199));
#43162=CARTESIAN_POINT('Ctrl Pts',(13.2863164700112,-7.26383348564869,-0.699646919261793));
#43163=CARTESIAN_POINT('Ctrl Pts',(13.2748173090023,-7.28486666222208,-0.57115245381317));
#43164=CARTESIAN_POINT('Ctrl Pts',(13.2664510227834,-7.30005980724128,-0.441563969171537));
#43165=CARTESIAN_POINT('Ctrl Pts',(13.2613042752927,-7.30939745578421,-0.311391073637702));
#43166=CARTESIAN_POINT('Ctrl Pts',(13.2561988309336,-7.31866016882124,-0.182262827807302));
#43167=CARTESIAN_POINT('Ctrl Pts',(13.2542614634095,-7.32216103446727,-0.0525595133519065));
#43168=CARTESIAN_POINT('Ctrl Pts',(13.2555318677529,-7.3198604598385,0.0772214321948015));
#43169=CARTESIAN_POINT('Ctrl Pts',(13.2563983335702,-7.31829137729713,0.16573715053459));
#43170=CARTESIAN_POINT('Ctrl Pts',(13.2587560588235,-7.31402308269219,0.254288981130321));
#43171=CARTESIAN_POINT('Ctrl Pts',(13.2626054360147,-7.30703628683439,0.342719102199534));
#43172=CARTESIAN_POINT('Ctrl Pts',(13.2684086950193,-7.29650310602066,0.476034927301568));
#43173=CARTESIAN_POINT('Ctrl Pts',(13.2775701666805,-7.2798543418706,0.608312350205377));
#43174=CARTESIAN_POINT('Ctrl Pts',(13.289943417625,-7.25719547792716,0.739057191237071));
#43175=CARTESIAN_POINT('Ctrl Pts',(13.300929037023,-7.23707775329776,0.8551392999939));
#43176=CARTESIAN_POINT('Ctrl Pts',(13.3144456587152,-7.21222189770271,0.970013302477615));
#43177=CARTESIAN_POINT('Ctrl Pts',(13.3303603014235,-7.18268588222769,1.08333333333334));
#43178=CARTESIAN_POINT('Origin',(13.892722748591,-3.17092330887735,3.20017169526122E-15));
#43179=CARTESIAN_POINT('',(15.1423033840733,-0.0114224867026808,1.08333333333334));
#43180=CARTESIAN_POINT('',(14.6487667980729,0.141522102769127,1.08333333333334));
#43181=CARTESIAN_POINT('Origin',(13.892722748591,-3.17092330887735,1.08333333333334));
#43182=CARTESIAN_POINT('',(15.1423033840733,-0.0114224867026808,-1.08333333333333));
#43183=CARTESIAN_POINT('Ctrl Pts',(15.1423033840733,-0.0114224867026917,
-1.08333333333333));
#43184=CARTESIAN_POINT('Ctrl Pts',(15.1423953499066,0.110492695607724,-0.727666221822789));
#43185=CARTESIAN_POINT('Ctrl Pts',(15.1413590080604,0.169498193350193,-0.352782973842772));
#43186=CARTESIAN_POINT('Ctrl Pts',(15.1413590080604,0.169498193350193,0.352782973842778));
#43187=CARTESIAN_POINT('Ctrl Pts',(15.1423953499066,0.110492695607724,0.727666221822797));
#43188=CARTESIAN_POINT('Ctrl Pts',(15.1423033840733,-0.0114224867026924,
1.08333333333334));
#43189=CARTESIAN_POINT('',(14.2484814298548,0.208031110850763,-1.08333333333333));
#43190=CARTESIAN_POINT('Origin',(13.892722748591,-3.17092330887735,-1.08333333333333));
#43191=CARTESIAN_POINT('',(14.2484814298548,0.208031110850763,1.08333333333334));
#43192=CARTESIAN_POINT('Ctrl Pts',(14.2484814298548,0.208031110850764,1.08333333333334));
#43193=CARTESIAN_POINT('Ctrl Pts',(14.2468058395578,0.322795758952199,0.725928647976585));
#43194=CARTESIAN_POINT('Ctrl Pts',(14.2449910310593,0.377796936249431,0.352039859176993));
#43195=CARTESIAN_POINT('Ctrl Pts',(14.2449910310593,0.37779693624943,-0.352039859176987));
#43196=CARTESIAN_POINT('Ctrl Pts',(14.2468058395578,0.322795758952199,-0.725928647976577));
#43197=CARTESIAN_POINT('Ctrl Pts',(14.2484814298548,0.208031110850765,-1.08333333333333));
#43198=CARTESIAN_POINT('Origin',(13.892722748591,-3.17092330887735,1.08333333333334));
#43199=CARTESIAN_POINT('',(13.1366786991091,-6.48336872052383,1.08333333333334));
#43200=CARTESIAN_POINT('Origin',(13.892722748591,-3.17092330887735,3.20017169526122E-15));
#43201=CARTESIAN_POINT('',(12.7471768669564,-6.36961395396396,1.08333333333334));
#43202=CARTESIAN_POINT('Origin',(13.892722748591,-3.17092330887735,1.08333333333334));
#43203=CARTESIAN_POINT('',(12.7471768669564,-6.36961395396396,-1.08333333333333));
#43204=CARTESIAN_POINT('Ctrl Pts',(12.7471768669564,-6.36961395396397,-1.08333333333334));
#43205=CARTESIAN_POINT('Ctrl Pts',(12.6958726976266,-6.47228631765585,-0.725928647976583));
#43206=CARTESIAN_POINT('Ctrl Pts',(12.6703734952067,-6.52105325020152,-0.352039859176989));
#43207=CARTESIAN_POINT('Ctrl Pts',(12.6703734952067,-6.52105325020152,3.73360976135914E-15));
#43208=CARTESIAN_POINT('Ctrl Pts',(12.6703734952067,-6.52105325020152,0.352039859176996));
#43209=CARTESIAN_POINT('Ctrl Pts',(12.6958726976266,-6.47228631765585,0.725928647976591));
#43210=CARTESIAN_POINT('Ctrl Pts',(12.7471768669564,-6.36961395396397,1.08333333333335));
#43211=CARTESIAN_POINT('',(13.6476999686242,-6.55970790622078,-1.08333333333333));
#43212=CARTESIAN_POINT('Origin',(13.892722748591,-3.17092330887735,-1.08333333333333));
#43213=CARTESIAN_POINT('',(13.6476999686242,-6.55970790622078,1.08333333333334));
#43214=CARTESIAN_POINT('Ctrl Pts',(13.6476999686242,-6.55970790622078,1.08333333333334));
#43215=CARTESIAN_POINT('Ctrl Pts',(13.5948858118209,-6.66958959248674,0.727666221822799));
#43216=CARTESIAN_POINT('Ctrl Pts',(13.5683505740919,-6.72230205711255,0.35278297384278));
#43217=CARTESIAN_POINT('Ctrl Pts',(13.5683505740919,-6.72230205711255,3.93962482987281E-15));
#43218=CARTESIAN_POINT('Ctrl Pts',(13.5683505740919,-6.72230205711255,-0.352782973842771));
#43219=CARTESIAN_POINT('Ctrl Pts',(13.5948858118209,-6.66958959248674,-0.72766622182279));
#43220=CARTESIAN_POINT('Ctrl Pts',(13.6476999686242,-6.55970790622078,-1.08333333333333));
#43221=CARTESIAN_POINT('Origin',(13.892722748591,-3.17092330887735,1.08333333333334));
#43222=CARTESIAN_POINT('',(13.0227870731057,-2.97236616780865,-3.45272288248773));
#43223=CARTESIAN_POINT('Origin',(13.0227870731057,-2.97236616780865,2.9997830762867E-15));
#43224=CARTESIAN_POINT('',(14.7626584240763,-3.36948044994605,-3.45272288248773));
#43225=CARTESIAN_POINT('Origin',(14.7626584240763,-3.36948044994605,3.40056031423575E-15));
#43226=CARTESIAN_POINT('Origin',(11.1410986251693,8.88472967648709,9.85584169237555E-16));
#43227=CARTESIAN_POINT('',(11.8387328710639,9.44107442276104,3.96060240207311));
#43228=CARTESIAN_POINT('Origin',(11.8387328710639,9.44107442276104,1.0472995612114E-15));
#43229=CARTESIAN_POINT('',(10.4434643792748,8.32838493021314,3.96060240207311));
#43230=CARTESIAN_POINT('Origin',(11.1410986251693,8.88472967648709,2.5198520116158));
#43231=CARTESIAN_POINT('Origin',(10.4434643792748,8.32838493021314,9.23868777263706E-16));
#43232=CARTESIAN_POINT('',(8.89378902201275,12.2552029391784,-1.08333333331655));
#43233=CARTESIAN_POINT('',(8.89378902201677,12.2552029391754,1.08333333333333));
#43234=CARTESIAN_POINT('Ctrl Pts',(8.89378902201274,12.2552029391784,-1.08333333331655));
#43235=CARTESIAN_POINT('Ctrl Pts',(8.86335293025879,12.2772908784853,-0.956315399884826));
#43236=CARTESIAN_POINT('Ctrl Pts',(8.83824313040494,12.2953456493747,-0.827586922367285));
#43237=CARTESIAN_POINT('Ctrl Pts',(8.81859777764014,12.3094197866805,-0.69766772380084));
#43238=CARTESIAN_POINT('Ctrl Pts',(8.7991879276401,12.3233252073292,-0.569305958731489));
#43239=CARTESIAN_POINT('Ctrl Pts',(8.78511225071473,12.3333449381983,-0.439781849534452));
#43240=CARTESIAN_POINT('Ctrl Pts',(8.77647376760361,12.3394890678296,-0.309596747993595));
#43241=CARTESIAN_POINT('Ctrl Pts',(8.76964787761092,12.344343988818,-0.206728088024587));
#43242=CARTESIAN_POINT('Ctrl Pts',(8.76621624622163,12.3467783236357,-0.103446722778746));
#43243=CARTESIAN_POINT('Ctrl Pts',(8.76621624622163,12.3467783236357,-7.54951656745106E-15));
#43244=CARTESIAN_POINT('Ctrl Pts',(8.76621624622163,12.3467783236357,0.130951008152141));
#43245=CARTESIAN_POINT('Ctrl Pts',(8.77171477448527,12.3428797767713,0.261548325668487));
#43246=CARTESIAN_POINT('Ctrl Pts',(8.78261416841303,12.3351194002049,0.391301356121213));
#43247=CARTESIAN_POINT('Ctrl Pts',(8.79368558213778,12.3272365454154,0.523102215114213));
#43248=CARTESIAN_POINT('Ctrl Pts',(8.81032969837903,12.3153689336875,0.654031926803563));
#43249=CARTESIAN_POINT('Ctrl Pts',(8.83241243050519,12.2995110840219,0.783576297698762));
#43250=CARTESIAN_POINT('Ctrl Pts',(8.84960195907419,12.2871670969504,0.88441557119687));
#43251=CARTESIAN_POINT('Ctrl Pts',(8.87008627043973,12.2724043900869,0.984415425401903));
#43252=CARTESIAN_POINT('Ctrl Pts',(8.89378902201675,12.2552029391755,1.08333333333333));
#43253=CARTESIAN_POINT('',(8.22258343557123,11.6383685130292,1.08333333333333));
#43254=CARTESIAN_POINT('Ctrl Pts',(8.89378902201675,12.2552029391755,1.08333333333333));
#43255=CARTESIAN_POINT('Ctrl Pts',(8.78751907456219,12.2023537225759,1.08333333333333));
#43256=CARTESIAN_POINT('Ctrl Pts',(8.68681488082489,12.1369760343758,1.08333333333333));
#43257=CARTESIAN_POINT('Ctrl Pts',(8.46069343470621,11.9566501984405,1.08333333333333));
#43258=CARTESIAN_POINT('Ctrl Pts',(8.31988542322917,11.7983921800676,1.08333333333333));
#43259=CARTESIAN_POINT('Ctrl Pts',(8.22258343557176,11.6383685130289,1.08333333333333));
#43260=CARTESIAN_POINT('',(8.22258343557175,11.6383685130288,-1.08333333333333));
#43261=CARTESIAN_POINT('Ctrl Pts',(8.2225834355717,11.6383685130289,1.08333333333318));
#43262=CARTESIAN_POINT('Ctrl Pts',(8.19448780675769,11.6582182584498,0.949301954017324));
#43263=CARTESIAN_POINT('Ctrl Pts',(8.17159767874311,11.6742430454627,0.81366496302888));
#43264=CARTESIAN_POINT('Ctrl Pts',(8.15402161030241,11.6865063889394,0.67695567866062));
#43265=CARTESIAN_POINT('Ctrl Pts',(8.13658119548769,11.6986750828637,0.541301528447691));
#43266=CARTESIAN_POINT('Ctrl Pts',(8.12437307855494,11.7071402381473,0.40459157308691));
#43267=CARTESIAN_POINT('Ctrl Pts',(8.1174733585697,11.7119223986889,0.26734687734235));
#43268=CARTESIAN_POINT('Ctrl Pts',(8.11300215046573,11.7150213700985,0.178408544025479));
#43269=CARTESIAN_POINT('Ctrl Pts',(8.11075954642938,11.7165728598428,0.0892456520429063));
#43270=CARTESIAN_POINT('Ctrl Pts',(8.11075954642938,11.7165728598428,-1.33226762955019E-15));
#43271=CARTESIAN_POINT('Ctrl Pts',(8.11075954642938,11.7165728598428,-0.137335411050026));
#43272=CARTESIAN_POINT('Ctrl Pts',(8.11607262981309,11.7129002012938,-0.274553571737022));
#43273=CARTESIAN_POINT('Ctrl Pts',(8.12665801674411,11.7055512249056,-0.411127959090392));
#43274=CARTESIAN_POINT('Ctrl Pts',(8.13729388250879,11.698167203246,-0.548353632582512));
#43275=CARTESIAN_POINT('Ctrl Pts',(8.15325248641432,11.6870716767896,-0.684929378140945));
#43276=CARTESIAN_POINT('Ctrl Pts',(8.17446212457132,11.6722178258439,-0.820321104282498));
#43277=CARTESIAN_POINT('Ctrl Pts',(8.18828255682692,11.6625388940673,-0.908543834215877));
#43278=CARTESIAN_POINT('Ctrl Pts',(8.20433194575505,11.6512633098961,-0.9962638332735));
#43279=CARTESIAN_POINT('Ctrl Pts',(8.22258343557176,11.6383685130288,-1.08333333333334));
#43280=CARTESIAN_POINT('Ctrl Pts',(8.89378902201473,12.2552029391744,-1.08333333333333));
#43281=CARTESIAN_POINT('Ctrl Pts',(8.7875190745609,12.202353722575,-1.08333333333333));
#43282=CARTESIAN_POINT('Ctrl Pts',(8.68681488082435,12.1369760343753,-1.08333333333333));
#43283=CARTESIAN_POINT('Ctrl Pts',(8.46069343470619,11.9566501984405,-1.08333333333333));
#43284=CARTESIAN_POINT('Ctrl Pts',(8.31988542322913,11.7983921800676,-1.08333333333333));
#43285=CARTESIAN_POINT('Ctrl Pts',(8.22258343557172,11.6383685130288,-1.08333333333333));
#43286=CARTESIAN_POINT('',(13.9269936544443,5.94376395877129,-1.08333333333333));
#43287=CARTESIAN_POINT('',(13.1762672612271,5.42664547033562,-1.08333333333333));
#43288=CARTESIAN_POINT('Ctrl Pts',(13.9269936544443,5.94376395877129,-1.08333333333333));
#43289=CARTESIAN_POINT('Ctrl Pts',(13.8517896638478,5.85187873682469,-1.08333333333333));
#43290=CARTESIAN_POINT('Ctrl Pts',(13.7657237213495,5.76832601371371,-1.08333333333333));
#43291=CARTESIAN_POINT('Ctrl Pts',(13.5395781511316,5.5879809394513,-1.08333333333333));
#43292=CARTESIAN_POINT('Ctrl Pts',(13.3544742809805,5.48608062863226,-1.08333333333333));
#43293=CARTESIAN_POINT('Ctrl Pts',(13.1762672612269,5.42664547033621,-1.08333333333333));
#43294=CARTESIAN_POINT('',(13.1762672612355,5.42664547033908,1.08333333333333));
#43295=CARTESIAN_POINT('Ctrl Pts',(13.1762672612269,5.42664547033617,1.08333333333318));
#43296=CARTESIAN_POINT('Ctrl Pts',(13.1893705593041,5.39482976422236,0.949270311030452));
#43297=CARTESIAN_POINT('Ctrl Pts',(13.1999097963792,5.36892368585892,0.813521288368082));
#43298=CARTESIAN_POINT('Ctrl Pts',(13.2079621630868,5.34904061477083,0.676607052101254));
#43299=CARTESIAN_POINT('Ctrl Pts',(13.2148460430323,5.33204279546023,0.559560573777983));
#43300=CARTESIAN_POINT('Ctrl Pts',(13.2199117356377,5.31944645364959,0.441662516279123));
#43301=CARTESIAN_POINT('Ctrl Pts',(13.2231796369647,5.31131059989547,0.323238258334714));
#43302=CARTESIAN_POINT('Ctrl Pts',(13.2269557156993,5.30190957419912,0.186398348762647));
#43303=CARTESIAN_POINT('Ctrl Pts',(13.2283213471703,5.2984924131362,0.0492519096262126));
#43304=CARTESIAN_POINT('Ctrl Pts',(13.2273014856384,5.30103720115497,-0.087675827066048));
#43305=CARTESIAN_POINT('Ctrl Pts',(13.2262786675026,5.30358936657715,-0.225000520654307));
#43306=CARTESIAN_POINT('Ctrl Pts',(13.22285647475,5.31213809759657,-0.362105241912749));
#43307=CARTESIAN_POINT('Ctrl Pts',(13.2170113253899,5.32664168351083,-0.498460177595588));
#43308=CARTESIAN_POINT('Ctrl Pts',(13.2111409592133,5.34120783998435,-0.635403368116607));
#43309=CARTESIAN_POINT('Ctrl Pts',(13.2028266475275,5.36178038996296,-0.771590289741134));
#43310=CARTESIAN_POINT('Ctrl Pts',(13.1919958930594,5.38829698119018,-0.906484242526414));
#43311=CARTESIAN_POINT('Ctrl Pts',(13.1872415508606,5.3999368857798,-0.965698216399684));
#43312=CARTESIAN_POINT('Ctrl Pts',(13.1820016856381,5.41272189470467,-1.02466304565381));
#43313=CARTESIAN_POINT('Ctrl Pts',(13.1762672612269,5.42664547033617,-1.08333333333318));
#43314=CARTESIAN_POINT('',(13.9269936544443,5.94376395877129,1.08333333333333));
#43315=CARTESIAN_POINT('Ctrl Pts',(13.9269936544443,5.94376395877129,1.08333333333333));
#43316=CARTESIAN_POINT('Ctrl Pts',(13.8517896638478,5.85187873682469,1.08333333333333));
#43317=CARTESIAN_POINT('Ctrl Pts',(13.7657237213495,5.76832601371371,1.08333333333333));
#43318=CARTESIAN_POINT('Ctrl Pts',(13.5395781511339,5.5879809394531,1.08333333333333));
#43319=CARTESIAN_POINT('Ctrl Pts',(13.3544742809865,5.48608062863536,1.08333333333333));
#43320=CARTESIAN_POINT('Ctrl Pts',(13.1762672612355,5.42664547033908,1.08333333333333));
#43321=CARTESIAN_POINT('Ctrl Pts',(13.9269936544443,5.9437639587713,-1.08333333333333));
#43322=CARTESIAN_POINT('Ctrl Pts',(13.9416885168395,5.90933203032488,-0.95688863210334));
#43323=CARTESIAN_POINT('Ctrl Pts',(13.9536527109305,5.88095561854266,-0.828820583351241));
#43324=CARTESIAN_POINT('Ctrl Pts',(13.9629765258053,5.85873440158633,-0.699646919261855));
#43325=CARTESIAN_POINT('Ctrl Pts',(13.9722513158077,5.83663002439342,-0.571152453813261));
#43326=CARTESIAN_POINT('Ctrl Pts',(13.9789135007645,5.82061622745854,-0.441563969171658));
#43327=CARTESIAN_POINT('Ctrl Pts',(13.9830050237944,5.81077040959811,-0.31139107363785));
#43328=CARTESIAN_POINT('Ctrl Pts',(13.987063711968,5.80100360535004,-0.182262827807452));
#43329=CARTESIAN_POINT('Ctrl Pts',(13.9885928700522,5.79730615639857,-0.0525595133520559));
#43330=CARTESIAN_POINT('Ctrl Pts',(13.9875862925321,5.79973378332923,0.077221432194654));
#43331=CARTESIAN_POINT('Ctrl Pts',(13.9868997670033,5.80138952054645,0.165737150534494));
#43332=CARTESIAN_POINT('Ctrl Pts',(13.9850326975557,5.80589410253397,0.254288981130278));
#43333=CARTESIAN_POINT('Ctrl Pts',(13.9819702480148,5.81325986277498,0.342719102199545));
#43334=CARTESIAN_POINT('Ctrl Pts',(13.977353348451,5.82436436418423,0.476034927301432));
#43335=CARTESIAN_POINT('Ctrl Pts',(13.9700489046451,5.84190742581571,0.608312350205104));
#43336=CARTESIAN_POINT('Ctrl Pts',(13.9600480872369,5.86570879353505,0.739057191236667));
#43337=CARTESIAN_POINT('Ctrl Pts',(13.9511688384277,5.88684089277784,0.855139299993628));
#43338=CARTESIAN_POINT('Ctrl Pts',(13.9401632237805,5.91290598563348,0.970013302477476));
#43339=CARTESIAN_POINT('Ctrl Pts',(13.9269936544443,5.9437639587713,1.08333333333333));
#43340=CARTESIAN_POINT('Origin',(11.1410986251693,8.88472967648709,9.85584169237555E-16));
#43341=CARTESIAN_POINT('',(8.72113759169208,11.2696166353064,1.08333333333333));
#43342=CARTESIAN_POINT('',(9.02271027299523,11.54110464988,1.08333333333333));
#43343=CARTESIAN_POINT('Origin',(11.1410986251693,8.88472967648709,1.08333333333333));
#43344=CARTESIAN_POINT('',(13.2594869773434,6.22835470309422,1.08333333333333));
#43345=CARTESIAN_POINT('Origin',(11.1410986251693,8.88472967648709,9.85584169237555E-16));
#43346=CARTESIAN_POINT('',(12.9276994994135,5.9947548451011,1.08333333333333));
#43347=CARTESIAN_POINT('Origin',(11.1410986251693,8.88472967648709,1.08333333333333));
#43348=CARTESIAN_POINT('',(12.9276994994135,5.9947548451011,-1.08333333333333));
#43349=CARTESIAN_POINT('Ctrl Pts',(12.9276994994135,5.9947548451011,-1.08333333333333));
#43350=CARTESIAN_POINT('Ctrl Pts',(12.9759843593573,5.89062845864264,-0.725928647976581));
#43351=CARTESIAN_POINT('Ctrl Pts',(12.9982133898606,5.84028669430273,-0.352039859176989));
#43352=CARTESIAN_POINT('Ctrl Pts',(12.9982133898606,5.84028669430273,9.85141416048961E-16));
#43353=CARTESIAN_POINT('Ctrl Pts',(12.9982133898606,5.84028669430273,0.35203985917699));
#43354=CARTESIAN_POINT('Ctrl Pts',(12.9759843593573,5.89062845864264,0.72592864797658));
#43355=CARTESIAN_POINT('Ctrl Pts',(12.9276994994135,5.9947548451011,1.08333333333333));
#43356=CARTESIAN_POINT('',(13.6377879061428,6.58029051604763,-1.08333333333333));
#43357=CARTESIAN_POINT('Origin',(11.1410986251693,8.88472967648709,-1.08333333333333));
#43358=CARTESIAN_POINT('',(13.6377879061428,6.58029051604763,1.08333333333333));
#43359=CARTESIAN_POINT('Ctrl Pts',(13.6377879061428,6.58029051604764,1.08333333333332));
#43360=CARTESIAN_POINT('Ctrl Pts',(13.6907677796515,6.47048863474093,0.727666221822788));
#43361=CARTESIAN_POINT('Ctrl Pts',(13.7154355939006,6.41687686636464,0.352782973842773));
#43362=CARTESIAN_POINT('Ctrl Pts',(13.7154355939006,6.41687686636464,9.86054494281319E-16));
#43363=CARTESIAN_POINT('Ctrl Pts',(13.7154355939006,6.41687686636464,-0.352782973842772));
#43364=CARTESIAN_POINT('Ctrl Pts',(13.6907677796515,6.47048863474094,-0.727666221822788));
#43365=CARTESIAN_POINT('Ctrl Pts',(13.6377879061428,6.58029051604764,-1.08333333333332));
#43366=CARTESIAN_POINT('Origin',(11.1410986251693,8.88472967648709,1.08333333333333));
#43367=CARTESIAN_POINT('',(9.4500021963329,11.8316076987797,1.08333333333333));
#43368=CARTESIAN_POINT('Origin',(11.1410986251693,8.88472967648709,1.08333333333333));
#43369=CARTESIAN_POINT('',(9.4500021963329,11.8316076987797,-1.08333333333333));
#43370=CARTESIAN_POINT('Ctrl Pts',(9.4500021963329,11.8316076987798,1.08333333333334));
#43371=CARTESIAN_POINT('Ctrl Pts',(9.35474240837097,11.9076924734258,0.7276662218228));
#43372=CARTESIAN_POINT('Ctrl Pts',(9.30796390402485,11.9436715548399,0.352782973842779));
#43373=CARTESIAN_POINT('Ctrl Pts',(9.30796390402485,11.9436715548399,-0.352782973842777));
#43374=CARTESIAN_POINT('Ctrl Pts',(9.35474240837097,11.9076924734258,-0.7276662218228));
#43375=CARTESIAN_POINT('Ctrl Pts',(9.4500021963329,11.8316076987798,-1.08333333333334));
#43376=CARTESIAN_POINT('',(8.72113759169208,11.2696166353064,-1.08333333333333));
#43377=CARTESIAN_POINT('Origin',(11.1410986251693,8.88472967648709,-1.08333333333333));
#43378=CARTESIAN_POINT('Ctrl Pts',(8.72113759169207,11.2696166353064,-1.08333333333334));
#43379=CARTESIAN_POINT('Ctrl Pts',(8.63036626326973,11.3398611937657,-0.725928647976583));
#43380=CARTESIAN_POINT('Ctrl Pts',(8.5862330966948,11.3727349924819,-0.35203985917699));
#43381=CARTESIAN_POINT('Ctrl Pts',(8.5862330966948,11.3727349924819,0.352039859176991));
#43382=CARTESIAN_POINT('Ctrl Pts',(8.63036626326973,11.3398611937657,0.725928647976584));
#43383=CARTESIAN_POINT('Ctrl Pts',(8.72113759169207,11.2696166353064,1.08333333333334));
#43384=CARTESIAN_POINT('',(10.4434643792748,8.32838493021314,-3.45272288248773));
#43385=CARTESIAN_POINT('Origin',(10.4434643792748,8.32838493021314,9.23868777263706E-16));
#43386=CARTESIAN_POINT('',(11.8387328710639,9.44107442276105,-3.45272288248773));
#43387=CARTESIAN_POINT('Origin',(11.8387328710639,9.44107442276104,1.0472995612114E-15));
#43388=CARTESIAN_POINT('Origin',(0.,14.25,0.));
#43389=CARTESIAN_POINT('',(-3.35834339016074,14.7651959662676,1.08333333333333));
#43390=CARTESIAN_POINT('',(-3.39763111739558,14.25,1.08333333333333));
#43391=CARTESIAN_POINT('Origin',(1.55588456152529E-16,14.25,1.08333333333333));
#43392=CARTESIAN_POINT('',(-3.35834339016074,14.7651959662676,-1.08333333333333));
#43393=CARTESIAN_POINT('Ctrl Pts',(-3.35834339016074,14.7651959662676,-1.08333333333333));
#43394=CARTESIAN_POINT('Ctrl Pts',(-3.47722236863702,14.7381569460943,-0.727666221822795));
#43395=CARTESIAN_POINT('Ctrl Pts',(-3.53451786760282,14.7240166290356,-0.352782973842776));
#43396=CARTESIAN_POINT('Ctrl Pts',(-3.53451786760282,14.7240166290356,0.352782973842775));
#43397=CARTESIAN_POINT('Ctrl Pts',(-3.47722236863702,14.7381569460943,0.727666221822794));
#43398=CARTESIAN_POINT('Ctrl Pts',(-3.35834339016074,14.7651959662676,1.08333333333333));
#43399=CARTESIAN_POINT('',(-3.37340073180097,13.8449509750914,-1.08333333333333));
#43400=CARTESIAN_POINT('Origin',(-1.5558845615253E-16,14.25,-1.08333333333333));
#43401=CARTESIAN_POINT('',(-3.37340073180097,13.8449509750914,1.08333333333333));
#43402=CARTESIAN_POINT('Ctrl Pts',(-3.37340073180098,13.8449509750914,1.08333333333333));
#43403=CARTESIAN_POINT('Ctrl Pts',(-3.48491513664897,13.8177798586608,0.725928647976578));
#43404=CARTESIAN_POINT('Ctrl Pts',(-3.53813348671686,13.8037716378594,0.352039859176988));
#43405=CARTESIAN_POINT('Ctrl Pts',(-3.53813348671686,13.8037716378594,-0.352039859176988));
#43406=CARTESIAN_POINT('Ctrl Pts',(-3.48491513664897,13.8177798586608,-0.725928647976578));
#43407=CARTESIAN_POINT('Ctrl Pts',(-3.37340073180098,13.8449509750914,-1.08333333333333));
#43408=CARTESIAN_POINT('Origin',(1.55588456152529E-16,14.25,1.08333333333333));
#43409=CARTESIAN_POINT('',(3.39763111739558,14.25,1.08333333333333));
#43410=CARTESIAN_POINT('Origin',(0.,14.25,0.));
#43411=CARTESIAN_POINT('',(3.37340073180097,13.8449509750914,1.08333333333333));
#43412=CARTESIAN_POINT('Origin',(0.,14.25,1.08333333333333));
#43413=CARTESIAN_POINT('',(3.37340073180097,13.8449509750914,-1.08333333333333));
#43414=CARTESIAN_POINT('Ctrl Pts',(3.37340073180098,13.8449509750914,-1.08333333333333));
#43415=CARTESIAN_POINT('Ctrl Pts',(3.48491513664897,13.8177798586608,-0.725928647976578));
#43416=CARTESIAN_POINT('Ctrl Pts',(3.53813348671686,13.8037716378594,-0.352039859176988));
#43417=CARTESIAN_POINT('Ctrl Pts',(3.53813348671686,13.8037716378594,0.));
#43418=CARTESIAN_POINT('Ctrl Pts',(3.53813348671686,13.8037716378594,0.352039859176988));
#43419=CARTESIAN_POINT('Ctrl Pts',(3.48491513664897,13.8177798586608,0.725928647976578));
#43420=CARTESIAN_POINT('Ctrl Pts',(3.37340073180098,13.8449509750914,1.08333333333333));
#43421=CARTESIAN_POINT('',(3.35834339016074,14.7651959662676,-1.08333333333333));
#43422=CARTESIAN_POINT('Origin',(0.,14.25,-1.08333333333333));
#43423=CARTESIAN_POINT('',(3.35834339016074,14.7651959662676,1.08333333333333));
#43424=CARTESIAN_POINT('Ctrl Pts',(3.35834339016074,14.7651959662676,1.08333333333333));
#43425=CARTESIAN_POINT('Ctrl Pts',(3.47722236863702,14.7381569460943,0.727666221822794));
#43426=CARTESIAN_POINT('Ctrl Pts',(3.53451786760282,14.7240166290356,0.352782973842775));
#43427=CARTESIAN_POINT('Ctrl Pts',(3.53451786760282,14.7240166290356,0.));
#43428=CARTESIAN_POINT('Ctrl Pts',(3.53451786760282,14.7240166290356,-0.352782973842775));
#43429=CARTESIAN_POINT('Ctrl Pts',(3.47722236863702,14.7381569460943,-0.727666221822793));
#43430=CARTESIAN_POINT('Ctrl Pts',(3.35834339016074,14.7651959662676,-1.08333333333333));
#43431=CARTESIAN_POINT('Origin',(0.,14.25,1.08333333333333));
#43432=CARTESIAN_POINT('',(0.,13.3576923076923,-3.45272288248773));
#43433=CARTESIAN_POINT('Origin',(0.,13.3576923076923,0.));
#43434=CARTESIAN_POINT('',(0.,15.1423076923077,-3.45272288248773));
#43435=CARTESIAN_POINT('Origin',(0.,15.1423076923077,0.));
#43436=CARTESIAN_POINT('Origin',(0.,14.25,0.));
#43437=CARTESIAN_POINT('',(-4.85033905439415E-16,15.1423076923077,3.96060240207311));
#43438=CARTESIAN_POINT('Origin',(0.,15.1423076923077,0.));
#43439=CARTESIAN_POINT('',(-4.85033905439415E-16,13.3576923076923,3.96060240207311));
#43440=CARTESIAN_POINT('Origin',(3.08592870035031E-16,14.25,2.5198520116158));
#43441=CARTESIAN_POINT('Origin',(0.,13.3576923076923,0.));
#43442=CARTESIAN_POINT('',(-3.97254599103887,13.6850786752975,-1.08333333333333));
#43443=CARTESIAN_POINT('',(-4.03631672677061,14.5944383081266,-1.08333333333333));
#43444=CARTESIAN_POINT('Ctrl Pts',(-3.97254599103889,13.6850786752975,-1.08333333333333));
#43445=CARTESIAN_POINT('Ctrl Pts',(-4.03699073486477,13.8609255570095,-1.08333333333333));
#43446=CARTESIAN_POINT('Ctrl Pts',(-4.07292947680577,14.0696859538838,-1.08333333333333));
#43447=CARTESIAN_POINT('Ctrl Pts',(-4.07292947680577,14.358906139038,-1.08333333333333));
#43448=CARTESIAN_POINT('Ctrl Pts',(-4.06125577389194,14.4784021699804,-1.08333333333333));
#43449=CARTESIAN_POINT('Ctrl Pts',(-4.03631672677123,14.5944383081267,-1.08333333333333));
#43450=CARTESIAN_POINT('',(-4.03631672677098,14.5944383081279,1.08333333333333));
#43451=CARTESIAN_POINT('Ctrl Pts',(-4.03631672677125,14.5944383081264,1.08333333333353));
#43452=CARTESIAN_POINT('Ctrl Pts',(-4.07239878927587,14.5844592579328,0.956888632103535));
#43453=CARTESIAN_POINT('Ctrl Pts',(-4.10204391436992,14.576120838176,0.828820583351431));
#43454=CARTESIAN_POINT('Ctrl Pts',(-4.12523046485396,14.5695557880246,0.699646919262042));
#43455=CARTESIAN_POINT('Ctrl Pts',(-4.14829509982461,14.5630252570856,0.571152453813459));
#43456=CARTESIAN_POINT('Ctrl Pts',(-4.16496899480084,14.5582495239489,0.441563969171867));
#43457=CARTESIAN_POINT('Ctrl Pts',(-4.17521778805797,14.555309638438,0.311391073638072));
#43458=CARTESIAN_POINT('Ctrl Pts',(-4.18538433378736,14.5523933457842,0.182262827807668));
#43459=CARTESIAN_POINT('Ctrl Pts',(-4.18922853025337,14.5512835680019,0.0525595133522669));
#43460=CARTESIAN_POINT('Ctrl Pts',(-4.18670294427272,14.5520101946411,-0.0772214321944475));
#43461=CARTESIAN_POINT('Ctrl Pts',(-4.18498039512374,14.5525057826387,-0.165737150534356));
#43462=CARTESIAN_POINT('Ctrl Pts',(-4.1802944723506,14.5538546098955,-0.254288981130209));
#43463=CARTESIAN_POINT('Ctrl Pts',(-4.17262628304436,14.5560527668241,-0.342719102199544));
#43464=CARTESIAN_POINT('Ctrl Pts',(-4.16106584445129,14.5593666727772,-0.476034927301542));
#43465=CARTESIAN_POINT('Ctrl Pts',(-4.14279588034764,14.5645937486684,-0.608312350205319));
#43466=CARTESIAN_POINT('Ctrl Pts',(-4.11795181407459,14.5716147048116,-0.739057191236983));
#43467=CARTESIAN_POINT('Ctrl Pts',(-4.09589395251526,14.5778482769217,-0.855139299993905));
#43468=CARTESIAN_POINT('Ctrl Pts',(-4.06865355383155,14.5854950604866,-0.970013302477714));
#43469=CARTESIAN_POINT('Ctrl Pts',(-4.03631672677125,14.5944383081264,-1.08333333333353));
#43470=CARTESIAN_POINT('',(-3.97254599103887,13.6850786752975,1.08333333333333));
#43471=CARTESIAN_POINT('Ctrl Pts',(-3.97254599103889,13.6850786752975,1.08333333333333));
#43472=CARTESIAN_POINT('Ctrl Pts',(-4.03718797255354,13.8614637488071,1.08333333333333));
#43473=CARTESIAN_POINT('Ctrl Pts',(-4.07292947680577,14.0697175866198,1.08333333333333));
#43474=CARTESIAN_POINT('Ctrl Pts',(-4.07292947680577,14.3589686276554,1.08333333333333));
#43475=CARTESIAN_POINT('Ctrl Pts',(-4.06126656486658,14.4783519618466,1.08333333333333));
#43476=CARTESIAN_POINT('Ctrl Pts',(-4.03631672677098,14.5944383081279,1.08333333333333));
#43477=CARTESIAN_POINT('Ctrl Pts',(-3.97254599103885,13.6850786752975,-1.08333333333333));
#43478=CARTESIAN_POINT('Ctrl Pts',(-4.0055902844374,13.6754864779574,-0.949270311030653));
#43479=CARTESIAN_POINT('Ctrl Pts',(-4.03241557892495,13.6675742096383,-0.813521288368336));
#43480=CARTESIAN_POINT('Ctrl Pts',(-4.05298135839275,13.6614729113855,-0.67660705210156));
#43481=CARTESIAN_POINT('Ctrl Pts',(-4.07056281760631,13.6562569784544,-0.559560573778188));
#43482=CARTESIAN_POINT('Ctrl Pts',(-4.08356944187665,13.6523638057542,-0.441662516279225));
#43483=CARTESIAN_POINT('Ctrl Pts',(-4.09196781162929,13.6498461320482,-0.32323825833471));
#43484=CARTESIAN_POINT('Ctrl Pts',(-4.10167217606822,13.6469369456345,-0.186398348762652));
#43485=CARTESIAN_POINT('Ctrl Pts',(-4.10519527746315,13.6458740742379,-0.0492519096262281));
#43486=CARTESIAN_POINT('Ctrl Pts',(-4.1025698088094,13.6466633637621,0.0876758270660229));
#43487=CARTESIAN_POINT('Ctrl Pts',(-4.09993672885708,13.6474549414561,0.225000520654293));
#43488=CARTESIAN_POINT('Ctrl Pts',(-4.0911193595297,13.6501094100325,0.362105241912746));
#43489=CARTESIAN_POINT('Ctrl Pts',(-4.07613560843688,13.6545823261509,0.498460177595596));
#43490=CARTESIAN_POINT('Ctrl Pts',(-4.06108721528303,13.659074539074,0.635403368116582));
#43491=CARTESIAN_POINT('Ctrl Pts',(-4.03981905948952,13.6654009235528,0.771590289741077));
#43492=CARTESIAN_POINT('Ctrl Pts',(-4.01233468870309,13.673465922941,0.906484242526326));
#43493=CARTESIAN_POINT('Ctrl Pts',(-4.00026996096645,13.6770061903378,0.965698216399675));
#43494=CARTESIAN_POINT('Ctrl Pts',(-3.98700723595603,13.6808808214243,1.02466304565388));
#43495=CARTESIAN_POINT('Ctrl Pts',(-3.97254599103885,13.6850786752975,1.08333333333333));
#43496=CARTESIAN_POINT('',(4.0363167267713,14.5944383081264,-1.08333333333333));
#43497=CARTESIAN_POINT('',(3.97254599103947,13.6850786752973,-1.08333333333333));
#43498=CARTESIAN_POINT('Ctrl Pts',(4.0363167267713,14.5944383081264,-1.08333333333333));
#43499=CARTESIAN_POINT('Ctrl Pts',(4.06125577389196,14.4784021699801,-1.08333333333333));
#43500=CARTESIAN_POINT('Ctrl Pts',(4.07292947680577,14.3589061390379,-1.08333333333333));
#43501=CARTESIAN_POINT('Ctrl Pts',(4.07292947680577,14.0696859538838,-1.08333333333333));
#43502=CARTESIAN_POINT('Ctrl Pts',(4.03699073486477,13.8609255570095,-1.08333333333333));
#43503=CARTESIAN_POINT('Ctrl Pts',(3.97254599103889,13.6850786752975,-1.08333333333333));
#43504=CARTESIAN_POINT('',(3.972545991042,13.685078675306,1.08333333333333));
#43505=CARTESIAN_POINT('Ctrl Pts',(3.97254599103891,13.6850786752974,1.08333333333318));
#43506=CARTESIAN_POINT('Ctrl Pts',(4.00550358468898,13.6755116454224,0.949622058007565));
#43507=CARTESIAN_POINT('Ctrl Pts',(4.03223833992508,13.667626413385,0.814376693553222));
#43508=CARTESIAN_POINT('Ctrl Pts',(4.05275116551691,13.6615412011384,0.678132403728152));
#43509=CARTESIAN_POINT('Ctrl Pts',(4.07316650047532,13.6554849098804,0.542535637670838));
#43510=CARTESIAN_POINT('Ctrl Pts',(4.0874189867075,13.6512115628239,0.40594941879892));
#43511=CARTESIAN_POINT('Ctrl Pts',(4.09549564973878,13.6487880554638,0.268901316711817));
#43512=CARTESIAN_POINT('Ctrl Pts',(4.10076932144717,13.6472056219574,0.179415511018788));
#43513=CARTESIAN_POINT('Ctrl Pts',(4.10340966592831,13.6464108509735,0.0897327832366672));
#43514=CARTESIAN_POINT('Ctrl Pts',(4.10340966592831,13.6464108509735,-4.66293670342566E-15));
#43515=CARTESIAN_POINT('Ctrl Pts',(4.10340966592831,13.6464108509735,-0.137573936980382));
#43516=CARTESIAN_POINT('Ctrl Pts',(4.09720533291532,13.6482810316174,-0.274951212619736));
#43517=CARTESIAN_POINT('Ctrl Pts',(4.08483748845152,13.6519816397819,-0.41161240621476));
#43518=CARTESIAN_POINT('Ctrl Pts',(4.07237395114171,13.6557108803995,-0.549330978772818));
#43519=CARTESIAN_POINT('Ctrl Pts',(4.05365110225785,13.6612989721827,-0.686322345436846));
#43520=CARTESIAN_POINT('Ctrl Pts',(4.02869583028489,13.6686542829587,-0.822054935347102));
#43521=CARTESIAN_POINT('Ctrl Pts',(4.01257796374822,13.6734048590114,-0.909720570537157));
#43522=CARTESIAN_POINT('Ctrl Pts',(3.99385994844905,13.6788915953345,-0.996861109122728));
#43523=CARTESIAN_POINT('Ctrl Pts',(3.97254599103891,13.6850786752974,-1.08333333333318));
#43524=CARTESIAN_POINT('',(4.0363167267713,14.5944383081264,1.08333333333333));
#43525=CARTESIAN_POINT('Ctrl Pts',(4.0363167267713,14.5944383081264,1.08333333333333));
#43526=CARTESIAN_POINT('Ctrl Pts',(4.06125577389196,14.4784021699801,1.08333333333333));
#43527=CARTESIAN_POINT('Ctrl Pts',(4.07292947680577,14.3589061390379,1.08333333333333));
#43528=CARTESIAN_POINT('Ctrl Pts',(4.07292947680577,14.0696859538867,1.08333333333333));
#43529=CARTESIAN_POINT('Ctrl Pts',(4.03699073486612,13.8609255570161,1.08333333333333));
#43530=CARTESIAN_POINT('Ctrl Pts',(3.97254599104201,13.685078675306,1.08333333333333));
#43531=CARTESIAN_POINT('Ctrl Pts',(4.0363167267713,14.5944383081264,-1.08333333333333));
#43532=CARTESIAN_POINT('Ctrl Pts',(4.07267660468553,14.5843824238018,-0.955915065626592));
#43533=CARTESIAN_POINT('Ctrl Pts',(4.10254364280131,14.5759803979714,-0.826701571450557));
#43534=CARTESIAN_POINT('Ctrl Pts',(4.12584816889326,14.5693808768856,-0.696211209492171));
#43535=CARTESIAN_POINT('Ctrl Pts',(4.14878536602558,14.5628853783063,-0.567777653525462));
#43536=CARTESIAN_POINT('Ctrl Pts',(4.16536539316191,14.5581360328796,-0.438107164856169));
#43537=CARTESIAN_POINT('Ctrl Pts',(4.17550906341001,14.5552260824043,-0.307693975181436));
#43538=CARTESIAN_POINT('Ctrl Pts',(4.18345734283739,14.55294593144,-0.205506064179161));
#43539=CARTESIAN_POINT('Ctrl Pts',(4.18745357006455,14.5517942140162,-0.102862147740973));
#43540=CARTESIAN_POINT('Ctrl Pts',(4.18745357006455,14.5517942140162,4.44089209850063E-16));
#43541=CARTESIAN_POINT('Ctrl Pts',(4.18745357006455,14.5517942140162,0.13066680730557));
#43542=CARTESIAN_POINT('Ctrl Pts',(4.18100368362964,14.5536548201376,0.261069786498731));
#43543=CARTESIAN_POINT('Ctrl Pts',(4.16817103415993,14.5573291670729,0.390710450871123));
#43544=CARTESIAN_POINT('Ctrl Pts',(4.15518429935153,14.561047632956,0.521907748246283));
#43545=CARTESIAN_POINT('Ctrl Pts',(4.13566054561854,14.5666236366129,0.652324314224272));
#43546=CARTESIAN_POINT('Ctrl Pts',(4.10965488440249,14.5739568744946,0.781443489202978));
#43547=CARTESIAN_POINT('Ctrl Pts',(4.08920880779353,14.5797223861759,0.882959098491578));
#43548=CARTESIAN_POINT('Ctrl Pts',(4.06475571708163,14.586573067282,0.983672743459539));
#43549=CARTESIAN_POINT('Ctrl Pts',(4.0363167267713,14.5944383081264,1.08333333333333));
#43550=CARTESIAN_POINT('Origin',(0.,0.,-1.08333333333333));
#43551=CARTESIAN_POINT('Origin',(0.,0.,1.08333333333333));
#43552=CARTESIAN_POINT('Origin',(0.,0.,-1.08333333333333));
#43553=CARTESIAN_POINT('Origin',(0.,0.,-1.08333333333333));
#43554=CARTESIAN_POINT('Origin',(0.,0.,-1.08333333333333));
#43555=CARTESIAN_POINT('Origin',(0.,0.,1.08333333333333));
#43556=CARTESIAN_POINT('Origin',(0.,0.,-1.08333333333333));
#43557=CARTESIAN_POINT('Origin',(0.,0.,1.08333333333333));
#43558=CARTESIAN_POINT('Origin',(0.,15.1423076923077,-3.45272288248773));
#43559=CARTESIAN_POINT('Origin',(0.,13.3576923076923,-3.45272288248773));
#43560=CARTESIAN_POINT('Origin',(0.,0.,-1.08333333333333));
#43561=CARTESIAN_POINT('Origin',(0.,0.,-1.08333333333333));
#43562=CARTESIAN_POINT('Origin',(0.,0.,-1.08333333333333));
#43563=CARTESIAN_POINT('Origin',(0.,0.,1.08333333333333));
#43564=CARTESIAN_POINT('Origin',(0.,0.,1.08333333333333));
#43565=CARTESIAN_POINT('Origin',(0.,0.,1.08333333333333));
#43566=CARTESIAN_POINT('Origin',(0.,0.,-1.08333333333333));
#43567=CARTESIAN_POINT('Origin',(0.,0.,-1.08333333333333));
#43568=CARTESIAN_POINT('Origin',(10.4434643792748,8.32838493021314,-3.45272288248773));
#43569=CARTESIAN_POINT('Origin',(11.8387328710639,9.44107442276104,-3.45272288248773));
#43570=CARTESIAN_POINT('Origin',(-1.55588456152528E-16,7.49274514625042E-17,
1.08333333333333));
#43571=CARTESIAN_POINT('Origin',(-1.55588456152528E-16,7.49274514625042E-17,
1.08333333333333));
#43572=CARTESIAN_POINT('Origin',(-1.55588456152528E-16,7.49274514625042E-17,
1.08333333333333));
#43573=CARTESIAN_POINT('Origin',(1.55588456152528E-16,-7.49274514625042E-17,
-1.08333333333333));
#43574=CARTESIAN_POINT('Origin',(1.55588456152528E-16,-7.49274514625042E-17,
-1.08333333333333));
#43575=CARTESIAN_POINT('Origin',(1.55588456152528E-16,-7.49274514625042E-17,
-1.08333333333333));
#43576=CARTESIAN_POINT('Origin',(1.55588456152528E-16,-7.49274514625042E-17,
-1.08333333333333));
#43577=CARTESIAN_POINT('Origin',(1.55588456152528E-16,-7.49274514625042E-17,
-1.08333333333333));
#43578=CARTESIAN_POINT('Origin',(1.94015631396094E-16,-2.43287906657286E-16,
-1.08333333333333));
#43579=CARTESIAN_POINT('Origin',(-1.94015631396094E-16,2.43287906657286E-16,
1.08333333333333));
#43580=CARTESIAN_POINT('Origin',(1.94015631396094E-16,-2.43287906657286E-16,
-1.08333333333333));
#43581=CARTESIAN_POINT('Origin',(1.94015631396094E-16,-2.43287906657286E-16,
-1.08333333333333));
#43582=CARTESIAN_POINT('Origin',(1.94015631396094E-16,-2.43287906657286E-16,
-1.08333333333333));
#43583=CARTESIAN_POINT('Origin',(-1.94015631396094E-16,2.43287906657286E-16,
1.08333333333333));
#43584=CARTESIAN_POINT('Origin',(-1.94015631396094E-16,2.43287906657286E-16,
1.08333333333333));
#43585=CARTESIAN_POINT('Origin',(1.94015631396094E-16,-2.43287906657286E-16,
-1.08333333333333));
#43586=CARTESIAN_POINT('Origin',(13.0227870731057,-2.97236616780865,-3.45272288248773));
#43587=CARTESIAN_POINT('Origin',(14.7626584240763,-3.36948044994605,-3.45272288248773));
#43588=CARTESIAN_POINT('Origin',(-1.94015631396094E-16,2.43287906657286E-16,
1.08333333333333));
#43589=CARTESIAN_POINT('Origin',(-1.94015631396094E-16,2.43287906657286E-16,
1.08333333333333));
#43590=CARTESIAN_POINT('Origin',(-1.94015631396094E-16,2.43287906657286E-16,
1.08333333333333));
#43591=CARTESIAN_POINT('Origin',(1.94015631396094E-16,-2.43287906657286E-16,
-1.08333333333333));
#43592=CARTESIAN_POINT('Origin',(1.94015631396094E-16,-2.43287906657286E-16,
-1.08333333333333));
#43593=CARTESIAN_POINT('Origin',(1.94015631396094E-16,-2.43287906657286E-16,
-1.08333333333333));
#43594=CARTESIAN_POINT('Origin',(1.94015631396094E-16,-2.43287906657286E-16,
-1.08333333333333));
#43595=CARTESIAN_POINT('Origin',(1.94015631396094E-16,-2.43287906657286E-16,
-1.08333333333333));
#43596=CARTESIAN_POINT('Origin',(8.63450790007668E-17,-3.78302508895262E-16,
-1.08333333333333));
#43597=CARTESIAN_POINT('Origin',(-8.63450790007668E-17,3.78302508895262E-16,
1.08333333333333));
#43598=CARTESIAN_POINT('Origin',(8.63450790007668E-17,-3.78302508895262E-16,
-1.08333333333333));
#43599=CARTESIAN_POINT('Origin',(8.63450790007668E-17,-3.78302508895262E-16,
-1.08333333333333));
#43600=CARTESIAN_POINT('Origin',(8.63450790007668E-17,-3.78302508895262E-16,
-1.08333333333333));
#43601=CARTESIAN_POINT('Origin',(-8.63450790007668E-17,3.78302508895262E-16,
1.08333333333333));
#43602=CARTESIAN_POINT('Origin',(-8.63450790007668E-17,3.78302508895262E-16,
1.08333333333333));
#43603=CARTESIAN_POINT('Origin',(8.63450790007668E-17,-3.78302508895262E-16,
-1.08333333333333));
#43604=CARTESIAN_POINT('Origin',(5.79568548444348,-12.0348649162504,-3.45272288248773));
#43605=CARTESIAN_POINT('Origin',(6.57000108040713,-13.6427478189685,-3.45272288248772));
#43606=CARTESIAN_POINT('Origin',(-8.63450790007668E-17,3.78302508895262E-16,
1.08333333333333));
#43607=CARTESIAN_POINT('Origin',(-8.63450790007668E-17,3.78302508895262E-16,
1.08333333333333));
#43608=CARTESIAN_POINT('Origin',(-8.63450790007668E-17,3.78302508895262E-16,
1.08333333333333));
#43609=CARTESIAN_POINT('Origin',(8.63450790007668E-17,-3.78302508895262E-16,
-1.08333333333333));
#43610=CARTESIAN_POINT('Origin',(8.63450790007668E-17,-3.78302508895262E-16,
-1.08333333333333));
#43611=CARTESIAN_POINT('Origin',(8.63450790007668E-17,-3.78302508895262E-16,
-1.08333333333333));
#43612=CARTESIAN_POINT('Origin',(8.63450790007668E-17,-3.78302508895262E-16,
-1.08333333333333));
#43613=CARTESIAN_POINT('Origin',(8.63450790007668E-17,-3.78302508895262E-16,
-1.08333333333333));
#43614=CARTESIAN_POINT('Origin',(-8.63450790007644E-17,-3.78302508895264E-16,
-1.08333333333333));
#43615=CARTESIAN_POINT('Origin',(8.63450790007644E-17,3.78302508895264E-16,
1.08333333333333));
#43616=CARTESIAN_POINT('Origin',(-8.63450790007644E-17,-3.78302508895264E-16,
-1.08333333333333));
#43617=CARTESIAN_POINT('Origin',(-8.63450790007644E-17,-3.78302508895264E-16,
-1.08333333333333));
#43618=CARTESIAN_POINT('Origin',(-8.63450790007644E-17,-3.78302508895264E-16,
-1.08333333333333));
#43619=CARTESIAN_POINT('Origin',(8.63450790007644E-17,3.78302508895264E-16,
1.08333333333333));
#43620=CARTESIAN_POINT('Origin',(8.63450790007644E-17,3.78302508895264E-16,
1.08333333333333));
#43621=CARTESIAN_POINT('Origin',(-8.63450790007644E-17,-3.78302508895264E-16,
-1.08333333333333));
#43622=CARTESIAN_POINT('Origin',(-5.79568548444331,-12.0348649162504,-3.45272288248773));
#43623=CARTESIAN_POINT('Origin',(-6.57000108040694,-13.6427478189686,-3.45272288248772));
#43624=CARTESIAN_POINT('Origin',(8.63450790007644E-17,3.78302508895264E-16,
1.08333333333333));
#43625=CARTESIAN_POINT('Origin',(8.63450790007644E-17,3.78302508895264E-16,
1.08333333333333));
#43626=CARTESIAN_POINT('Origin',(8.63450790007644E-17,3.78302508895264E-16,
1.08333333333333));
#43627=CARTESIAN_POINT('Origin',(-8.63450790007644E-17,-3.78302508895264E-16,
-1.08333333333333));
#43628=CARTESIAN_POINT('Origin',(-8.63450790007644E-17,-3.78302508895264E-16,
-1.08333333333333));
#43629=CARTESIAN_POINT('Origin',(-8.63450790007644E-17,-3.78302508895264E-16,
-1.08333333333333));
#43630=CARTESIAN_POINT('Origin',(-8.63450790007644E-17,-3.78302508895264E-16,
-1.08333333333333));
#43631=CARTESIAN_POINT('Origin',(-8.63450790007644E-17,-3.78302508895264E-16,
-1.08333333333333));
#43632=CARTESIAN_POINT('Origin',(-1.94015631396093E-16,-2.43287906657289E-16,
-1.08333333333333));
#43633=CARTESIAN_POINT('Origin',(1.94015631396093E-16,2.43287906657289E-16,
1.08333333333333));
#43634=CARTESIAN_POINT('Origin',(-1.94015631396093E-16,-2.43287906657289E-16,
-1.08333333333333));
#43635=CARTESIAN_POINT('Origin',(-1.94015631396093E-16,-2.43287906657289E-16,
-1.08333333333333));
#43636=CARTESIAN_POINT('Origin',(-1.94015631396093E-16,-2.43287906657289E-16,
-1.08333333333333));
#43637=CARTESIAN_POINT('Origin',(1.94015631396093E-16,2.43287906657289E-16,
1.08333333333333));
#43638=CARTESIAN_POINT('Origin',(1.94015631396093E-16,2.43287906657289E-16,
1.08333333333333));
#43639=CARTESIAN_POINT('Origin',(-1.94015631396093E-16,-2.43287906657289E-16,
-1.08333333333333));
#43640=CARTESIAN_POINT('Origin',(-13.0227870731057,-2.97236616780882,-3.45272288248773));
#43641=CARTESIAN_POINT('Origin',(-14.7626584240763,-3.36948044994625,-3.45272288248773));
#43642=CARTESIAN_POINT('Origin',(1.94015631396093E-16,2.43287906657289E-16,
1.08333333333333));
#43643=CARTESIAN_POINT('Origin',(1.94015631396093E-16,2.43287906657289E-16,
1.08333333333333));
#43644=CARTESIAN_POINT('Origin',(1.94015631396093E-16,2.43287906657289E-16,
1.08333333333333));
#43645=CARTESIAN_POINT('Origin',(-1.94015631396093E-16,-2.43287906657289E-16,
-1.08333333333333));
#43646=CARTESIAN_POINT('Origin',(-1.94015631396093E-16,-2.43287906657289E-16,
-1.08333333333333));
#43647=CARTESIAN_POINT('Origin',(-1.94015631396093E-16,-2.43287906657289E-16,
-1.08333333333333));
#43648=CARTESIAN_POINT('Origin',(-1.94015631396093E-16,-2.43287906657289E-16,
-1.08333333333333));
#43649=CARTESIAN_POINT('Origin',(-1.94015631396093E-16,-2.43287906657289E-16,
-1.08333333333333));
#43650=CARTESIAN_POINT('Origin',(-1.55588456152529E-16,-7.49274514625064E-17,
-1.08333333333333));
#43651=CARTESIAN_POINT('Origin',(1.55588456152529E-16,7.49274514625064E-17,
1.08333333333333));
#43652=CARTESIAN_POINT('Origin',(-1.55588456152529E-16,-7.49274514625064E-17,
-1.08333333333333));
#43653=CARTESIAN_POINT('Origin',(-1.55588456152529E-16,-7.49274514625064E-17,
-1.08333333333333));
#43654=CARTESIAN_POINT('Origin',(-1.55588456152529E-16,-7.49274514625064E-17,
-1.08333333333333));
#43655=CARTESIAN_POINT('Origin',(1.55588456152529E-16,7.49274514625064E-17,
1.08333333333333));
#43656=CARTESIAN_POINT('Origin',(1.55588456152529E-16,7.49274514625064E-17,
1.08333333333333));
#43657=CARTESIAN_POINT('Origin',(-1.55588456152529E-16,-7.49274514625064E-17,
-1.08333333333333));
#43658=CARTESIAN_POINT('Origin',(-10.4434643792749,8.32838493021299,-3.45272288248773));
#43659=CARTESIAN_POINT('Origin',(-11.838732871064,9.44107442276088,-3.45272288248773));
#43660=CARTESIAN_POINT('Origin',(1.55588456152529E-16,7.49274514625064E-17,
1.08333333333333));
#43661=CARTESIAN_POINT('Origin',(1.55588456152529E-16,7.49274514625064E-17,
1.08333333333333));
#43662=CARTESIAN_POINT('Origin',(1.55588456152529E-16,7.49274514625064E-17,
1.08333333333333));
#43663=CARTESIAN_POINT('Origin',(-1.55588456152529E-16,-7.49274514625064E-17,
-1.08333333333333));
#43664=CARTESIAN_POINT('Origin',(-1.55588456152529E-16,-7.49274514625064E-17,
-1.08333333333333));
#43665=CARTESIAN_POINT('Origin',(-1.55588456152529E-16,-7.49274514625064E-17,
-1.08333333333333));
#43666=CARTESIAN_POINT('Origin',(-1.55588456152529E-16,-7.49274514625064E-17,
-1.08333333333333));
#43667=CARTESIAN_POINT('Origin',(-1.55588456152529E-16,-7.49274514625064E-17,
-1.08333333333333));
#43668=CARTESIAN_POINT('Origin',(0.,0.,-1.08333333333333));
#43669=CARTESIAN_POINT('Origin',(0.,0.,-1.08333333333333));
#43670=CARTESIAN_POINT('Origin',(0.,0.,-1.08333333333333));
#43671=CARTESIAN_POINT('Origin',(0.,0.,1.08333333333333));
#43672=CARTESIAN_POINT('Origin',(0.,0.,1.08333333333333));
#43673=CARTESIAN_POINT('Origin',(0.,0.,1.08333333333333));
#43674=CARTESIAN_POINT('Origin',(0.,0.,-1.08333333333333));
#43675=CARTESIAN_POINT('Origin',(0.,0.,-1.08333333333333));
#43768=UNCERTAINTY_MEASURE_WITH_UNIT(LENGTH_MEASURE(0.01),#43782,
'DISTANCE_ACCURACY_VALUE',
'Maximum model space distance between geometric entities at asserted c
onnectivities');
#43771=UNCERTAINTY_MEASURE_WITH_UNIT(LENGTH_MEASURE(0.01),#43782,
'DISTANCE_ACCURACY_VALUE',
'Maximum model space distance between geometric entities at asserted c
onnectivities');
#43778=(
GEOMETRIC_REPRESENTATION_CONTEXT(3)
GLOBAL_UNCERTAINTY_ASSIGNED_CONTEXT((#43768))
GLOBAL_UNIT_ASSIGNED_CONTEXT((#43782,#43784,#43785))
REPRESENTATION_CONTEXT('','3D')
);
#43781=(
GEOMETRIC_REPRESENTATION_CONTEXT(3)
GLOBAL_UNCERTAINTY_ASSIGNED_CONTEXT((#43771))
GLOBAL_UNIT_ASSIGNED_CONTEXT((#43782,#43784,#43785))
REPRESENTATION_CONTEXT('','3D')
);
#43782=(
LENGTH_UNIT()
NAMED_UNIT(*)
SI_UNIT(.MILLI.,.METRE.)
);
#43784=(
NAMED_UNIT(*)
PLANE_ANGLE_UNIT()
SI_UNIT($,.RADIAN.)
);
#43785=(
NAMED_UNIT(*)
SI_UNIT($,.STERADIAN.)
SOLID_ANGLE_UNIT()
);
#43792=SHAPE_DEFINITION_REPRESENTATION(#43801,#43818);
#43801=PRODUCT_DEFINITION_SHAPE('',$,#43828);
#43818=SHAPE_REPRESENTATION('',(#14566),#43778);
#43821=PRODUCT_DEFINITION_CONTEXT('part definition',#43850,'design');
#43828=PRODUCT_DEFINITION('5972K117_Steel Ball Bearing_3','Bearing_04',
#43837,#43821);
#43837=PRODUCT_DEFINITION_FORMATION('',$,#43858);
#43850=APPLICATION_CONTEXT(
'Core Data for Automotive Mechanical Design Process');
#43851=PRODUCT_CONTEXT('part definition',#43850,'mechanical');
#43858=PRODUCT('5972K117_Steel Ball Bearing_3','Bearing_04',$,(#43851));
#43863=PRESENTATION_STYLE_ASSIGNMENT((#43866));
#43866=SURFACE_STYLE_USAGE(.BOTH.,#43869);
#43869=SURFACE_SIDE_STYLE('',(#43872));
#43872=SURFACE_STYLE_FILL_AREA(#43875);
#43875=FILL_AREA_STYLE('Opaque(160,160,160)',(#43878));
#43878=FILL_AREA_STYLE_COLOUR('Opaque(160,160,160)',#43881);
#43881=COLOUR_RGB('Opaque(160,160,160)', 0.31764706, 0.68627451, 0.89019608);
ENDSEC;
END-ISO-10303-21;
